ISO-10303-21;
HEADER;
FILE_DESCRIPTION (('STEP AP214'),
    '1' );
FILE_NAME ('Upper Tension Leaf Spring.step',
    '2026-10-06T10:23:46',
    ( '' ),
    ( '' ),
    'SwSTEP 2.0',
    'SolidWorks 2020',
    '' );
FILE_SCHEMA (( 'AUTOMOTIVE_DESIGN' ));
ENDSEC;

DATA;
#17=DIRECTION ( 'NONE',  ( -9.925461516413211857E-16, 0.8967398287344598984, 0.4425581086832454658 ) ) ;
#30=VERTEX_POINT ( 'NONE', #22566 ) ;
#32=EDGE_CURVE ( 'NONE', #20252, #1331, #16766, .T. ) ;
#52=CARTESIAN_POINT ( 'NONE',  ( 38.31606138205700773, -22.27515649656512053, 29.48506754039017963 ) ) ;
#72=LINE ( 'NONE', #4208, #11613 ) ;
#126=VERTEX_POINT ( 'NONE', #6729 ) ;
#144=LINE ( 'NONE', #15861, #20989 ) ;
#162=ORIENTED_EDGE ( 'NONE', *, *, #2908, .T. ) ;
#169=ORIENTED_EDGE ( 'NONE', *, *, #3276, .T. ) ;
#242=DIRECTION ( 'NONE',  ( 1.218693434051482139E-16, -0.4425581086832393041, 0.8967398287344630070 ) ) ;
#253=DIRECTION ( 'NONE',  ( 1.000000000000000275E-15, -0.9439899321577401858, -0.3299742535180970604 ) ) ;
#265=LINE ( 'NONE', #13690, #19298 ) ;
#289=ORIENTED_EDGE ( 'NONE', *, *, #17382, .F. ) ;
#309=CARTESIAN_POINT ( 'NONE',  ( 37.14448850680319225, -21.82678658219787948, 29.70634659473178374 ) ) ;
#323=LINE ( 'NONE', #12708, #17156 ) ;
#356=AXIS2_PLACEMENT_3D ( 'NONE', #9538, #13647, #7988 ) ;
#368=FACE_OUTER_BOUND ( 'NONE', #16968, .T. ) ;
#369=AXIS2_PLACEMENT_3D ( 'NONE', #5770, #5638, #19552 ) ;
#378=AXIS2_PLACEMENT_3D ( 'NONE', #5265, #13131, #6123 ) ;
#400=ORIENTED_EDGE ( 'NONE', *, *, #21408, .T. ) ;
#421=ORIENTED_EDGE ( 'NONE', *, *, #16949, .T. ) ;
#454=AXIS2_PLACEMENT_3D ( 'NONE', #10382, #13746, #10009 ) ;
#477=EDGE_CURVE ( 'NONE', #16296, #2532, #6909, .T. ) ;
#482=CARTESIAN_POINT ( 'NONE',  ( 40.31606138205701484, -21.38339321089542011, 27.67811916372966863 ) ) ;
#497=PLANE ( 'NONE',  #7863 ) ;
#506=ADVANCED_FACE ( 'NONE', ( #12517 ), #18548, .T. ) ;
#546=VERTEX_POINT ( 'NONE', #873 ) ;
#568=ORIENTED_EDGE ( 'NONE', *, *, #2920, .F. ) ;
#569=ORIENTED_EDGE ( 'NONE', *, *, #16312, .T. ) ;
#639=LINE ( 'NONE', #22551, #16599 ) ;
#659=ORIENTED_EDGE ( 'NONE', *, *, #11638, .T. ) ;
#669=FACE_OUTER_BOUND ( 'NONE', #20627, .T. ) ;
#679=ORIENTED_EDGE ( 'NONE', *, *, #2955, .F. ) ;
#734=CIRCLE ( 'NONE', #8109, 0.7500000000000021094 ) ;
#754=CARTESIAN_POINT ( 'NONE',  ( 40.31606138205700773, -13.25716901376042323, 21.21736665487721041 ) ) ;
#760=CARTESIAN_POINT ( 'NONE',  ( 43.31606138205700773, -18.80550481115970740, 25.27912300651437150 ) ) ;
#772=LINE ( 'NONE', #24338, #9040 ) ;
#791=CIRCLE ( 'NONE', #19318, 2.000000000000001776 ) ;
#799=EDGE_CURVE ( 'NONE', #12627, #3377, #20490, .T. ) ;
#807=PLANE ( 'NONE',  #2853 ) ;
#827=EDGE_LOOP ( 'NONE', ( #8817, #12206, #569, #6532 ) ) ;
#828=VERTEX_POINT ( 'NONE', #10781 ) ;
#831=AXIS2_PLACEMENT_3D ( 'NONE', #7687, #10004, #9635 ) ;
#873=CARTESIAN_POINT ( 'NONE',  ( 40.31606138205700773, -12.40281258615395821, 20.95421293576468358 ) ) ;
#874=VERTEX_POINT ( 'NONE', #24530 ) ;
#890=EDGE_CURVE ( 'NONE', #20252, #9149, #6911, .T. ) ;
#899=ORIENTED_EDGE ( 'NONE', *, *, #20502, .F. ) ;
#915=CYLINDRICAL_SURFACE ( 'NONE', #21603, 3.000000000000000444 ) ;
#993=DIRECTION ( 'NONE',  ( 7.071067811865491110E-16, -0.9008287146801832179, 0.4341746501209495790 ) ) ;
#1018=( LENGTH_UNIT ( ) NAMED_UNIT ( * ) SI_UNIT ( .MILLI., .METRE. ) );
#1030=VERTEX_POINT ( 'NONE', #25162 ) ;
#1032=ADVANCED_FACE ( 'NONE', ( #7804 ), #17472, .F. ) ;
#1054=DIRECTION ( 'NONE',  ( 0.000000000000000000, -0.3299742535181005021, 0.9439899321577387425 ) ) ;
#1062=DIRECTION ( 'NONE',  ( -9.925461516413221718E-16, 0.8967398287344632291, 0.4425581086832394151 ) ) ;
#1081=EDGE_CURVE ( 'NONE', #11722, #2503, #12273, .T. ) ;
#1150=CARTESIAN_POINT ( 'NONE',  ( 33.31606138205700773, -19.73594837544667513, 24.33996001444790025 ) ) ;
#1168=CARTESIAN_POINT ( 'NONE',  ( 40.31606138205700773, -10.19550266980813014, 14.63954348514304904 ) ) ;
#1213=DIRECTION ( 'NONE',  ( -1.000000000000000078E-15, 0.9439899321577400748, 0.3299742535180970049 ) ) ;
#1221=EDGE_CURVE ( 'NONE', #7327, #16296, #2262, .T. ) ;
#1235=EDGE_CURVE ( 'NONE', #1331, #1701, #323, .T. ) ;
#1311=CARTESIAN_POINT ( 'NONE',  ( 33.31606138205700773, -21.39087554181784512, 28.82307548518892304 ) ) ;
#1331=VERTEX_POINT ( 'NONE', #14748 ) ;
#1339=EDGE_LOOP ( 'NONE', ( #19131, #24920, #3494, #3969 ) ) ;
#1343=PLANE ( 'NONE',  #12552 ) ;
#1351=ADVANCED_FACE ( 'NONE', ( #6774 ), #24897, .T. ) ;
#1373=CARTESIAN_POINT ( 'NONE',  ( 39.48763425731081611, -22.27515649656511343, 29.48506754039016542 ) ) ;
#1386=DIRECTION ( 'NONE',  ( 9.925461516413221718E-16, -0.8967398287344632291, -0.4425581086832394151 ) ) ;
#1414=CARTESIAN_POINT ( 'NONE',  ( 33.31606138205700773, -18.80550481115971806, 25.27912300651437150 ) ) ;
#1421=EDGE_CURVE ( 'NONE', #5245, #8986, #7540, .T. ) ;
#1422=CARTESIAN_POINT ( 'NONE',  ( 39.48763425731081611, -22.27515649656511343, 29.48506754039016897 ) ) ;
#1460=CARTESIAN_POINT ( 'NONE',  ( 33.31606138205700773, -13.58280000135114030, 20.54174511886706256 ) ) ;
#1478=EDGE_LOOP ( 'NONE', ( #2621, #21518, #17245, #2091 ) ) ;
#1486=DIRECTION ( 'NONE',  ( 7.071067811865491110E-16, -0.9008287146801832179, 0.4341746501209495790 ) ) ;
#1490=EDGE_LOOP ( 'NONE', ( #25234, #19392, #19945, #9121 ) ) ;
#1507=ORIENTED_EDGE ( 'NONE', *, *, #799, .T. ) ;
#1517=CARTESIAN_POINT ( 'NONE',  ( 36.31606138205700773, -19.13113579875042092, 24.60350147050422720 ) ) ;
#1533=LINE ( 'NONE', #24854, #22186 ) ;
#1534=DIRECTION ( 'NONE',  ( -1.000000000000000000, -1.000000000000000078E-15, 0.000000000000000000 ) ) ;
#1557=VECTOR ( 'NONE', #8982, 1000.000000000000000 ) ;
#1562=PRODUCT_CONTEXT ( 'NONE', #16705, 'mechanical' ) ;
#1573=CYLINDRICAL_SURFACE ( 'NONE', #3825, 1.250000000000000888 ) ;
#1579=DIRECTION ( 'NONE',  ( 0.000000000000000000, -0.3299742535180969494, 0.9439899321577399638 ) ) ;
#1597=CARTESIAN_POINT ( 'NONE',  ( 33.31606138205700773, -21.83924545618511104, 28.60179643084731893 ) ) ;
#1621=DIRECTION ( 'NONE',  ( 0.000000000000000000, 0.3299742535180963943, -0.9439899321577402969 ) ) ;
#1633=EDGE_LOOP ( 'NONE', ( #3458, #9690, #15478, #1507 ) ) ;
#1662=PRODUCT ( 'Upper Tension Leaf Spring', 'Upper Tension Leaf Spring', '', ( #1562 ) ) ;
#1670=EDGE_LOOP ( 'NONE', ( #19907, #18202, #22450, #14186 ) ) ;
#1701=VERTEX_POINT ( 'NONE', #18342 ) ;
#1718=CARTESIAN_POINT ( 'NONE',  ( 36.31606138205700773, -19.92642959707778516, 24.72592537066031682 ) ) ;
#1799=DIRECTION ( 'NONE',  ( -1.000000000000000000, -1.052872940142565459E-15, -1.848188032574765003E-17 ) ) ;
#1802=ORIENTED_EDGE ( 'NONE', *, *, #9504, .F. ) ;
#1810=LINE ( 'NONE', #17806, #24738 ) ;
#1833=LINE ( 'NONE', #11394, #15762 ) ;
#1841=LINE ( 'NONE', #11533, #13931 ) ;
#1845=DIRECTION ( 'NONE',  ( -1.218693434051482139E-16, 0.4425581086832393041, -0.8967398287344630070 ) ) ;
#1881=EDGE_CURVE ( 'NONE', #5254, #8221, #734, .T. ) ;
#1901=ADVANCED_FACE ( 'NONE', ( #2723 ), #6992, .T. ) ;
#1925=DIRECTION ( 'NONE',  ( -1.000000000000000000, -1.000000000000000078E-15, 0.000000000000000000 ) ) ;
#1956=DIRECTION ( 'NONE',  ( -1.000000000000000000, -1.000000000000000078E-15, 0.000000000000000000 ) ) ;
#1995=PLANE ( 'NONE',  #831 ) ;
#2000=AXIS2_PLACEMENT_3D ( 'NONE', #9286, #12766, #22537 ) ;
#2087=DIRECTION ( 'NONE',  ( 1.000000000000000275E-15, -0.9439899321577401858, -0.3299742535180970604 ) ) ;
#2091=ORIENTED_EDGE ( 'NONE', *, *, #12176, .F. ) ;
#2095=EDGE_LOOP ( 'NONE', ( #21744, #20124, #14575, #12917 ) ) ;
#2105=DIRECTION ( 'NONE',  ( -1.000000000000000000, -1.000000000000000078E-15, 0.000000000000000000 ) ) ;
#2131=VECTOR ( 'NONE', #1486, 1000.000000000000227 ) ;
#2218=VECTOR ( 'NONE', #11281, 1000.000000000000227 ) ;
#2232=VERTEX_POINT ( 'NONE', #4048 ) ;
#2241=FACE_OUTER_BOUND ( 'NONE', #11521, .T. ) ;
#2247=DIRECTION ( 'NONE',  ( 0.000000000000000000, 0.3299742535180922864, -0.9439899321577417401 ) ) ;
#2250=CARTESIAN_POINT ( 'NONE',  ( 38.31606138205700773, -21.82678658219787948, 29.70634659473178019 ) ) ;
#2262=LINE ( 'NONE', #10389, #24934 ) ;
#2263=ORIENTED_EDGE ( 'NONE', *, *, #23409, .T. ) ;
#2284=ORIENTED_EDGE ( 'NONE', *, *, #890, .T. ) ;
#2303=ORIENTED_EDGE ( 'NONE', *, *, #25191, .T. ) ;
#2326=DIRECTION ( 'NONE',  ( 1.000000000000000000, 1.000000000000000078E-15, 0.000000000000000000 ) ) ;
#2382=ORIENTED_EDGE ( 'NONE', *, *, #25220, .F. ) ;
#2411=COLOUR_RGB ( '', 0.66274510, 0.83137255, 0.94901961) ;
#2415=CIRCLE ( 'NONE', #11489, 1.250000000000000888 ) ;
#2437=CARTESIAN_POINT ( 'NONE',  ( 43.31606138205700063, -12.87480755223282358, 20.78922580900563588 ) ) ;
#2468=EDGE_CURVE ( 'NONE', #9599, #12562, #16016, .T. ) ;
#2486=VECTOR ( 'NONE', #242, 1000.000000000000227 ) ;
#2503=VERTEX_POINT ( 'NONE', #10991 ) ;
#2517=LINE ( 'NONE', #6151, #23965 ) ;
#2532=VERTEX_POINT ( 'NONE', #24368 ) ;
#2538=CARTESIAN_POINT ( 'NONE',  ( 36.31606138205700773, -23.16691978223482096, 31.29201591705069063 ) ) ;
#2545=CARTESIAN_POINT ( 'NONE',  ( 43.31606138205700063, -13.04008168869994222, 21.66778101221729713 ) ) ;
#2564=VERTEX_POINT ( 'NONE', #5323 ) ;
#2615=( GEOMETRIC_REPRESENTATION_CONTEXT ( 3 ) GLOBAL_UNCERTAINTY_ASSIGNED_CONTEXT ( ( #18541 ) ) GLOBAL_UNIT_ASSIGNED_CONTEXT ( ( #13905, #21761, #17912 ) ) REPRESENTATION_CONTEXT ( 'NONE', 'WORKASPACE' ) );
#2621=ORIENTED_EDGE ( 'NONE', *, *, #5162, .T. ) ;
#2634=CARTESIAN_POINT ( 'NONE',  ( 40.31606138205701484, -21.83924545618510393, 28.60179643084731893 ) ) ;
#2640=EDGE_LOOP ( 'NONE', ( #20648, #25357, #18740, #12834 ) ) ;
#2657=ORIENTED_EDGE ( 'NONE', *, *, #14433, .F. ) ;
#2658=DIRECTION ( 'NONE',  ( 1.218693434051482139E-16, -0.4425581086832393041, 0.8967398287344630070 ) ) ;
#2703=CIRCLE ( 'NONE', #15053, 0.7500000000000008882 ) ;
#2713=DIRECTION ( 'NONE',  ( 0.000000000000000000, 0.3299742535180963943, -0.9439899321577402969 ) ) ;
#2723=FACE_OUTER_BOUND ( 'NONE', #3679, .T. ) ;
#2734=CARTESIAN_POINT ( 'NONE',  ( 43.31606138205700773, -23.16691978223481385, 31.29201591705069063 ) ) ;
#2741=ORIENTED_EDGE ( 'NONE', *, *, #9787, .F. ) ;
#2752=CLOSED_SHELL ( 'NONE', ( #8944, #6499, #5802, #8149, #15544, #6122, #16293, #22483, #5295, #15406, #19827, #21250, #19368, #23304, #25048, #16019, #16902, #9415, #15719, #5696, #23420, #5063, #20436, #5386, #1351, #506, #1901, #11860, #13780, #9037, #1032, #21074, #16026, #12568, #10832, #22777, #15249, #14248, #4837, #22034, #14011, #8171, #11324, #24115, #17290 ) ) ;
#2798=DIRECTION ( 'NONE',  ( 1.000000000000000000, 1.000000000000000078E-15, 0.000000000000000000 ) ) ;
#2829=DIRECTION ( 'NONE',  ( 7.071067811865460542E-16, -0.4341746501209495790, -0.9008287146801832179 ) ) ;
#2836=EDGE_LOOP ( 'NONE', ( #15757, #8570, #14018, #16670, #21693, #4211, #10031, #23447, #14005, #10769 ) ) ;
#2853=AXIS2_PLACEMENT_3D ( 'NONE', #16665, #12814, #4810 ) ;
#2865=EDGE_LOOP ( 'NONE', ( #9354, #11043, #24760, #8527 ) ) ;
#2876=VERTEX_POINT ( 'NONE', #13938 ) ;
#2879=CARTESIAN_POINT ( 'NONE',  ( 43.31606138205700063, -13.58280000135112964, 20.54174511886706256 ) ) ;
#2887=ORIENTED_EDGE ( 'NONE', *, *, #1881, .T. ) ;
#2908=EDGE_CURVE ( 'NONE', #9564, #7327, #10326, .T. ) ;
#2920=EDGE_CURVE ( 'NONE', #9149, #30, #21694, .T. ) ;
#2945=VECTOR ( 'NONE', #9886, 1000.000000000000227 ) ;
#2955=EDGE_CURVE ( 'NONE', #8986, #12061, #11890, .T. ) ;
#2958=EDGE_CURVE ( 'NONE', #3261, #24591, #144, .T. ) ;
#2970=DIRECTION ( 'NONE',  ( 4.341746501209495972E-16, -0.4341746501209495790, -0.9008287146801833289 ) ) ;
#3002=VECTOR ( 'NONE', #12937, 1000.000000000000227 ) ;
#3010=FACE_OUTER_BOUND ( 'NONE', #13087, .T. ) ;
#3054=ORIENTED_EDGE ( 'NONE', *, *, #14434, .T. ) ;
#3078=CARTESIAN_POINT ( 'NONE',  ( 36.31606138205700063, -12.76023008545320714, 21.53290024082827969 ) ) ;
#3115=CARTESIAN_POINT ( 'NONE',  ( 43.31606138205700773, -19.34822312381089660, 24.15308711316412627 ) ) ;
#3198=PLANE ( 'NONE',  #16484 ) ;
#3208=SURFACE_SIDE_STYLE ('',( #7340 ) ) ;
#3221=VECTOR ( 'NONE', #17519, 1000.000000000000000 ) ;
#3227=ORIENTED_EDGE ( 'NONE', *, *, #22923, .T. ) ;
#3261=VERTEX_POINT ( 'NONE', #11475 ) ;
#3269=ORIENTED_EDGE ( 'NONE', *, *, #16792, .T. ) ;
#3272=ORIENTED_EDGE ( 'NONE', *, *, #8457, .F. ) ;
#3276=EDGE_CURVE ( 'NONE', #9062, #3532, #2415, .T. ) ;
#3277=CIRCLE ( 'NONE', #369, 3.000000000000002665 ) ;
#3309=CIRCLE ( 'NONE', #4127, 1.250000000000000888 ) ;
#3312=VERTEX_POINT ( 'NONE', #19316 ) ;
#3334=ORIENTED_EDGE ( 'NONE', *, *, #8960, .T. ) ;
#3339=EDGE_CURVE ( 'NONE', #12061, #126, #5720, .T. ) ;
#3377=VERTEX_POINT ( 'NONE', #2545 ) ;
#3401=CARTESIAN_POINT ( 'NONE',  ( 40.31606138205701484, -21.38339321089542011, 27.67811916372966863 ) ) ;
#3402=DIRECTION ( 'NONE',  ( -1.000000000000000000, -1.000000000000000078E-15, 0.000000000000000000 ) ) ;
#3418=LINE ( 'NONE', #9361, #12475 ) ;
#3458=ORIENTED_EDGE ( 'NONE', *, *, #25191, .F. ) ;
#3494=ORIENTED_EDGE ( 'NONE', *, *, #20044, .F. ) ;
#3525=ORIENTED_EDGE ( 'NONE', *, *, #18398, .T. ) ;
#3528=CARTESIAN_POINT ( 'NONE',  ( 36.31606138205700773, -23.16691978223482096, 31.29201591705069063 ) ) ;
#3532=VERTEX_POINT ( 'NONE', #12998 ) ;
#3544=ORIENTED_EDGE ( 'NONE', *, *, #32, .F. ) ;
#3548=DIRECTION ( 'NONE',  ( 9.925461516413211857E-16, -0.8967398287344598984, -0.4425581086832454658 ) ) ;
#3610=PLANE ( 'NONE',  #14417 ) ;
#3615=CARTESIAN_POINT ( 'NONE',  ( 43.31606138205700063, -13.58280000135112964, 20.54174511886706256 ) ) ;
#3618=DIRECTION ( 'NONE',  ( -1.000000000000000000, -1.000000000000000078E-15, 0.000000000000000000 ) ) ;
#3646=DIRECTION ( 'NONE',  ( -1.000000000000000000, -1.000000000000000078E-15, 0.000000000000000000 ) ) ;
#3679=EDGE_LOOP ( 'NONE', ( #21342, #2303, #5473, #14109 ) ) ;
#3744=DIRECTION ( 'NONE',  ( 0.000000000000000000, -0.3299742535180970049, 0.9439899321577400748 ) ) ;
#3769=LINE ( 'NONE', #21179, #9893 ) ;
#3770=DIRECTION ( 'NONE',  ( 7.071067811865460542E-16, -0.4341746501209495790, -0.9008287146801832179 ) ) ;
#3812=ORIENTED_EDGE ( 'NONE', *, *, #19506, .F. ) ;
#3816=AXIS2_PLACEMENT_3D ( 'NONE', #24713, #13019, #20872 ) ;
#3825=AXIS2_PLACEMENT_3D ( 'NONE', #19613, #1956, #21181 ) ;
#3831=DIRECTION ( 'NONE',  ( 1.000000000000000000, 8.911169920151748851E-16, 3.114923731923493702E-16 ) ) ;
#3906=DIRECTION ( 'NONE',  ( -1.000000000000000000, -1.000000000000000078E-15, 0.000000000000000000 ) ) ;
#3930=ORIENTED_EDGE ( 'NONE', *, *, #12883, .T. ) ;
#3945=FACE_OUTER_BOUND ( 'NONE', #10813, .T. ) ;
#3966=ORIENTED_EDGE ( 'NONE', *, *, #13822, .F. ) ;
#3969=ORIENTED_EDGE ( 'NONE', *, *, #8801, .F. ) ;
#3972=CARTESIAN_POINT ( 'NONE',  ( 43.31606138205700063, -12.97731741051367393, 21.08248588348817876 ) ) ;
#3975=LINE ( 'NONE', #24950, #10933 ) ;
#3985=CIRCLE ( 'NONE', #8941, 0.7500000000000021094 ) ;
#4014=DIRECTION ( 'NONE',  ( 0.000000000000000000, -0.4425581086832455213, 0.8967398287344598984 ) ) ;
#4030=CARTESIAN_POINT ( 'NONE',  ( 43.31606138205700773, -15.54379676492717621, 15.94803270339611245 ) ) ;
#4048=CARTESIAN_POINT ( 'NONE',  ( 43.31606138205700773, -19.92642959707777806, 24.72592537066031682 ) ) ;
#4086=( GEOMETRIC_REPRESENTATION_CONTEXT ( 3 ) GLOBAL_UNCERTAINTY_ASSIGNED_CONTEXT ( ( #23888 ) ) GLOBAL_UNIT_ASSIGNED_CONTEXT ( ( #1018, #18940, #17135 ) ) REPRESENTATION_CONTEXT ( 'NONE', 'WORKASPACE' ) );
#4127=AXIS2_PLACEMENT_3D ( 'NONE', #13795, #1925, #5678 ) ;
#4148=DIRECTION ( 'NONE',  ( -1.000000000000000000, -1.000000000000000078E-15, 0.000000000000000000 ) ) ;
#4186=LINE ( 'NONE', #12055, #23798 ) ;
#4200=ORIENTED_EDGE ( 'NONE', *, *, #5162, .F. ) ;
#4208=CARTESIAN_POINT ( 'NONE',  ( 40.31606138205700773, -12.97731741051367749, 21.08248588348817876 ) ) ;
#4211=ORIENTED_EDGE ( 'NONE', *, *, #4558, .F. ) ;
#4241=CARTESIAN_POINT ( 'NONE',  ( 40.31606138205700773, -19.13113579875042092, 24.60350147050422720 ) ) ;
#4266=CARTESIAN_POINT ( 'NONE',  ( 40.31606138205701484, -19.73594837544667158, 24.33996001444790025 ) ) ;
#4291=( GEOMETRIC_REPRESENTATION_CONTEXT ( 3 ) GLOBAL_UNCERTAINTY_ASSIGNED_CONTEXT ( ( #21115 ) ) GLOBAL_UNIT_ASSIGNED_CONTEXT ( ( #22616, #24062, #6431 ) ) REPRESENTATION_CONTEXT ( 'NONE', 'WORKASPACE' ) );
#4293=EDGE_LOOP ( 'NONE', ( #679, #5264, #5043, #14768 ) ) ;
#4304=EDGE_CURVE ( 'NONE', #19911, #5245, #14067, .T. ) ;
#4321=VECTOR ( 'NONE', #20645, 1000.000000000000114 ) ;
#4324=DIRECTION ( 'NONE',  ( -1.000000000000000000, -1.000000000000000078E-15, 0.000000000000000000 ) ) ;
#4351=CARTESIAN_POINT ( 'NONE',  ( 33.31606138205700773, -19.47805968271055477, 24.94720442500192448 ) ) ;
#4397=DIRECTION ( 'NONE',  ( -1.000000000000000000, -1.000000000000000078E-15, 0.000000000000000000 ) ) ;
#4401=EDGE_CURVE ( 'NONE', #24591, #828, #8634, .T. ) ;
#4413=VECTOR ( 'NONE', #8060, 1000.000000000000114 ) ;
#4433=AXIS2_PLACEMENT_3D ( 'NONE', #8401, #4531, #16241 ) ;
#4448=AXIS2_PLACEMENT_3D ( 'NONE', #6566, #8641, #12765 ) ;
#4479=EDGE_CURVE ( 'NONE', #15276, #874, #791, .T. ) ;
#4495=CARTESIAN_POINT ( 'NONE',  ( 43.31606138205700063, -12.87480755223282358, 20.78922580900563588 ) ) ;
#4531=DIRECTION ( 'NONE',  ( -1.000000000000000275E-15, 0.9439899321577401858, 0.3299742535180970604 ) ) ;
#4537=ORIENTED_EDGE ( 'NONE', *, *, #14464, .T. ) ;
#4540=EDGE_LOOP ( 'NONE', ( #4982, #20958, #20483, #6221 ) ) ;
#4547=VERTEX_POINT ( 'NONE', #13328 ) ;
#4558=EDGE_CURVE ( 'NONE', #3312, #4547, #5761, .T. ) ;
#4594=AXIS2_PLACEMENT_3D ( 'NONE', #6636, #20810, #10642 ) ;
#4601=EDGE_CURVE ( 'NONE', #3377, #9564, #3769, .T. ) ;
#4606=EDGE_LOOP ( 'NONE', ( #25096, #21984, #5612, #12063 ) ) ;
#4608=VECTOR ( 'NONE', #13640, 1000.000000000000227 ) ;
#4643=EDGE_CURVE ( 'NONE', #16021, #12836, #9715, .T. ) ;
#4646=FACE_OUTER_BOUND ( 'NONE', #21078, .T. ) ;
#4669=CYLINDRICAL_SURFACE ( 'NONE', #17777, 0.7500000000000008882 ) ;
#4674=CARTESIAN_POINT ( 'NONE',  ( 43.31606138205700773, -19.47805968271054766, 24.94720442500192448 ) ) ;
#4708=ORIENTED_EDGE ( 'NONE', *, *, #16496, .F. ) ;
#4720=ORIENTED_EDGE ( 'NONE', *, *, #32, .T. ) ;
#4765=EDGE_CURVE ( 'NONE', #16021, #9628, #14080, .T. ) ;
#4803=AXIS2_PLACEMENT_3D ( 'NONE', #21321, #21081, #15651 ) ;
#4810=DIRECTION ( 'NONE',  ( -1.000000000000000078E-15, 0.9439899321577400748, 0.3299742535180970049 ) ) ;
#4837=ADVANCED_FACE ( 'NONE', ( #14963 ), #9058, .T. ) ;
#4842=DIRECTION ( 'NONE',  ( 0.000000000000000000, -0.3299742535180970049, 0.9439899321577400748 ) ) ;
#4846=EDGE_CURVE ( 'NONE', #2503, #12061, #24473, .T. ) ;
#4910=AXIS2_PLACEMENT_3D ( 'NONE', #8470, #6528, #16190 ) ;
#4918=ORIENTED_EDGE ( 'NONE', *, *, #2958, .T. ) ;
#4919=DIRECTION ( 'NONE',  ( 1.000000000000000000, 1.000000000000000078E-15, 0.000000000000000000 ) ) ;
#4931=LINE ( 'NONE', #1311, #4321 ) ;
#4982=ORIENTED_EDGE ( 'NONE', *, *, #1221, .F. ) ;
#4999=PLANE ( 'NONE',  #14091 ) ;
#5018=EDGE_LOOP ( 'NONE', ( #2263, #9777, #15405, #4537 ) ) ;
#5029=VECTOR ( 'NONE', #2658, 1000.000000000000227 ) ;
#5043=ORIENTED_EDGE ( 'NONE', *, *, #7696, .F. ) ;
#5063=ADVANCED_FACE ( 'NONE', ( #23448 ), #3610, .T. ) ;
#5069=AXIS2_PLACEMENT_3D ( 'NONE', #16132, #6363, #10347 ) ;
#5072=CARTESIAN_POINT ( 'NONE',  ( 36.31606138205700063, -10.66749763588700262, 14.47455635838400134 ) ) ;
#5147=ORIENTED_EDGE ( 'NONE', *, *, #17756, .T. ) ;
#5162=EDGE_CURVE ( 'NONE', #16232, #24915, #3309, .T. ) ;
#5210=DIRECTION ( 'NONE',  ( 0.000000000000000000, 0.3299742535180963943, -0.9439899321577402969 ) ) ;
#5220=DIRECTION ( 'NONE',  ( 0.000000000000000000, -0.3299742535180970049, 0.9439899321577400748 ) ) ;
#5228=PLANE ( 'NONE',  #16560 ) ;
#5242=EDGE_CURVE ( 'NONE', #23347, #2532, #18302, .T. ) ;
#5245=VERTEX_POINT ( 'NONE', #19975 ) ;
#5246=EDGE_CURVE ( 'NONE', #2532, #11164, #18048, .T. ) ;
#5254=VERTEX_POINT ( 'NONE', #20222 ) ;
#5260=AXIS2_PLACEMENT_3D ( 'NONE', #11442, #1386, #22893 ) ;
#5264=ORIENTED_EDGE ( 'NONE', *, *, #1421, .F. ) ;
#5265=CARTESIAN_POINT ( 'NONE',  ( 38.31606138205700063, -11.51539968388051882, 18.41550321377400934 ) ) ;
#5295=ADVANCED_FACE ( 'NONE', ( #368 ), #497, .T. ) ;
#5323=CARTESIAN_POINT ( 'NONE',  ( 36.31606138205700063, -12.87480755223283246, 20.78922580900563588 ) ) ;
#5338=DIRECTION ( 'NONE',  ( -1.000000000000000000, -1.000000000000000078E-15, 0.000000000000000000 ) ) ;
#5345=DIRECTION ( 'NONE',  ( 0.000000000000000000, 0.3299742535180963943, -0.9439899321577402969 ) ) ;
#5349=VECTOR ( 'NONE', #6650, 1000.000000000000000 ) ;
#5350=DIRECTION ( 'NONE',  ( 9.925461516413211857E-16, -0.8967398287344598984, -0.4425581086832454658 ) ) ;
#5360=ORIENTED_EDGE ( 'NONE', *, *, #18074, .F. ) ;
#5361=VECTOR ( 'NONE', #12412, 1000.000000000000227 ) ;
#5371=LINE ( 'NONE', #14770, #6267 ) ;
#5386=ADVANCED_FACE ( 'NONE', ( #12632 ), #3198, .T. ) ;
#5396=ORIENTED_EDGE ( 'NONE', *, *, #7696, .T. ) ;
#5438=CARTESIAN_POINT ( 'NONE',  ( 37.14448850680319225, -21.82678658219788304, 29.70634659473178374 ) ) ;
#5455=EDGE_LOOP ( 'NONE', ( #3930, #20016, #2657, #16724 ) ) ;
#5463=ORIENTED_EDGE ( 'NONE', *, *, #25288, .F. ) ;
#5465=DIRECTION ( 'NONE',  ( -1.000000000000000078E-15, 0.9439899321577400748, 0.3299742535180970049 ) ) ;
#5473=ORIENTED_EDGE ( 'NONE', *, *, #17933, .T. ) ;
#5492=ORIENTED_EDGE ( 'NONE', *, *, #477, .F. ) ;
#5516=VECTOR ( 'NONE', #15565, 1000.000000000000227 ) ;
#5549=LINE ( 'NONE', #9426, #13990 ) ;
#5564=PLANE ( 'NONE',  #11684 ) ;
#5584=ORIENTED_EDGE ( 'NONE', *, *, #15612, .F. ) ;
#5592=FACE_OUTER_BOUND ( 'NONE', #15594, .T. ) ;
#5612=ORIENTED_EDGE ( 'NONE', *, *, #14434, .F. ) ;
#5638=DIRECTION ( 'NONE',  ( -1.000000000000000275E-15, 0.9439899321577401858, 0.3299742535180970604 ) ) ;
#5678=DIRECTION ( 'NONE',  ( 0.000000000000000000, 0.3299742535180974490, -0.9439899321577398528 ) ) ;
#5696=ADVANCED_FACE ( 'NONE', ( #3945 ), #1995, .T. ) ;
#5700=EDGE_CURVE ( 'NONE', #24520, #19911, #11251, .T. ) ;
#5720=CIRCLE ( 'NONE', #6949, 1.250000000000000888 ) ;
#5742=ORIENTED_EDGE ( 'NONE', *, *, #6302, .F. ) ;
#5744=VECTOR ( 'NONE', #24529, 1000.000000000000000 ) ;
#5761=CIRCLE ( 'NONE', #13181, 2.000000000000001776 ) ;
#5770=CARTESIAN_POINT ( 'NONE',  ( 40.31606138205700773, -11.18542543036241987, 17.47151328161626793 ) ) ;
#5802=ADVANCED_FACE ( 'NONE', ( #8709 ), #6511, .T. ) ;
#5829=DIRECTION ( 'NONE',  ( 1.000000000000000000, 1.000000000000000078E-15, 0.000000000000000000 ) ) ;
#5842=ORIENTED_EDGE ( 'NONE', *, *, #1081, .T. ) ;
#5900=EDGE_CURVE ( 'NONE', #11164, #24520, #21058, .T. ) ;
#5901=AXIS2_PLACEMENT_3D ( 'NONE', #15760, #23350, #23619 ) ;
#5955=CIRCLE ( 'NONE', #24033, 3.000000000000002220 ) ;
#5961=DIRECTION ( 'NONE',  ( 0.000000000000000000, -0.3299742535180974490, 0.9439899321577398528 ) ) ;
#6001=CARTESIAN_POINT ( 'NONE',  ( 36.31606138205700773, -18.80550481115971451, 25.27912300651437150 ) ) ;
#6035=ORIENTED_EDGE ( 'NONE', *, *, #17103, .F. ) ;
#6064=DIRECTION ( 'NONE',  ( 1.000000000000000000, 8.911169920151748851E-16, 3.114923731923493702E-16 ) ) ;
#6122=ADVANCED_FACE ( 'NONE', ( #5592 ), #19883, .T. ) ;
#6123=DIRECTION ( 'NONE',  ( 1.000000000000000000, 8.673617379884027583E-16, 0.000000000000000000 ) ) ;
#6151=CARTESIAN_POINT ( 'NONE',  ( 43.31606138205700063, -13.25716901376041967, 21.21736665487721041 ) ) ;
#6172=( BOUNDED_SURFACE ( )  B_SPLINE_SURFACE ( 3, 1, ( 
 ( #17042, #11373 ),
 ( #13551, #7757 ),
 ( #5438, #21539 ),
 ( #23199, #15349 ) ),
 .UNSPECIFIED., .F., .F., .T. ) 
 B_SPLINE_SURFACE_WITH_KNOTS ( ( 4, 4 ),
 ( 2, 2 ),
 ( 0.000000000000000000, 1.000000000000000000 ),
 ( 0.000000000000000000, 1.000000000000000000 ),
 .UNSPECIFIED. ) 
 GEOMETRIC_REPRESENTATION_ITEM ( )  RATIONAL_B_SPLINE_SURFACE ( (
 ( 1.000000000000000000, 1.000000000000000000),
 ( 0.8047378541243649375, 0.8047378541243649375),
 ( 0.8047378541243649375, 0.8047378541243649375),
 ( 1.000000000000000000, 1.000000000000000000) ) ) 
 REPRESENTATION_ITEM ( '' )  SURFACE ( )  );
#6175=LINE ( 'NONE', #7989, #16555 ) ;
#6204=CARTESIAN_POINT ( 'NONE',  ( 36.31606138205700063, -13.58280000135113674, 20.54174511886706256 ) ) ;
#6221=ORIENTED_EDGE ( 'NONE', *, *, #7705, .T. ) ;
#6229=LINE ( 'NONE', #10103, #20300 ) ;
#6233=PRODUCT_DEFINITION_SHAPE ( 'NONE', 'NONE',  #20652 ) ;
#6267=VECTOR ( 'NONE', #14892, 1000.000000000000227 ) ;
#6302=EDGE_CURVE ( 'NONE', #8221, #23347, #10481, .T. ) ;
#6307=CARTESIAN_POINT ( 'NONE',  ( 33.31606138205700773, -13.04008168869995288, 21.66778101221729713 ) ) ;
#6363=DIRECTION ( 'NONE',  ( -3.299742535180970203E-16, 0.3299742535180970049, -0.9439899321577400748 ) ) ;
#6408=DIRECTION ( 'NONE',  ( -1.000000000000000000, -1.000000000000000078E-15, 0.000000000000000000 ) ) ;
#6410=DIRECTION ( 'NONE',  ( 1.000000000000000000, 8.911169920151748851E-16, 3.114923731923493702E-16 ) ) ;
#6431=( NAMED_UNIT ( * ) SI_UNIT ( $, .STERADIAN. ) SOLID_ANGLE_UNIT ( ) );
#6448=ORIENTED_EDGE ( 'NONE', *, *, #477, .T. ) ;
#6499=ADVANCED_FACE ( 'NONE', ( #18578 ), #915, .T. ) ;
#6511=CYLINDRICAL_SURFACE ( 'NONE', #7452, 3.000000000000002665 ) ;
#6512=DIRECTION ( 'NONE',  ( -1.000000000000000000, -1.000000000000000078E-15, 0.000000000000000000 ) ) ;
#6528=DIRECTION ( 'NONE',  ( 1.000000000000000275E-15, -0.9439899321577400748, -0.3299742535180970049 ) ) ;
#6532=ORIENTED_EDGE ( 'NONE', *, *, #8385, .T. ) ;
#6556=CARTESIAN_POINT ( 'NONE',  ( 43.31606138205700063, -12.76023008545320181, 21.53290024082827969 ) ) ;
#6566=CARTESIAN_POINT ( 'NONE',  ( 40.31606138205700773, -18.80550481115971095, 25.27912300651437150 ) ) ;
#6619=CARTESIAN_POINT ( 'NONE',  ( 40.31606138205700773, -21.90577604921433874, 28.73660501626934760 ) ) ;
#6636=CARTESIAN_POINT ( 'NONE',  ( 33.31606138205700773, -18.80550481115971806, 25.27912300651437150 ) ) ;
#6650=DIRECTION ( 'NONE',  ( -1.000000000000000000, -1.000000000000000078E-15, 0.000000000000000000 ) ) ;
#6690=LINE ( 'NONE', #2437, #11062 ) ;
#6706=AXIS2_PLACEMENT_3D ( 'NONE', #18065, #12022, #22044 ) ;
#6719=ORIENTED_EDGE ( 'NONE', *, *, #890, .F. ) ;
#6729=CARTESIAN_POINT ( 'NONE',  ( 36.31606138205700773, -19.34822312381090370, 24.15308711316412627 ) ) ;
#6735=CARTESIAN_POINT ( 'NONE',  ( 36.31606138205700773, -21.38339321089542722, 27.67811916372966863 ) ) ;
#6736=CARTESIAN_POINT ( 'NONE',  ( 40.31606138205701484, -21.39087554181786643, 28.82307548518891238 ) ) ;
#6774=FACE_OUTER_BOUND ( 'NONE', #9714, .T. ) ;
#6821=DIRECTION ( 'NONE',  ( 0.000000000000000000, -0.3299742535180970049, 0.9439899321577400748 ) ) ;
#6909=CIRCLE ( 'NONE', #4448, 1.250000000000000888 ) ;
#6911=LINE ( 'NONE', #12844, #1557 ) ;
#6949=AXIS2_PLACEMENT_3D ( 'NONE', #9542, #17390, #23686 ) ;
#6966=LINE ( 'NONE', #1150, #22366 ) ;
#6992=PLANE ( 'NONE',  #16744 ) ;
#7010=FACE_OUTER_BOUND ( 'NONE', #24853, .T. ) ;
#7089=VERTEX_POINT ( 'NONE', #1517 ) ;
#7118=FACE_OUTER_BOUND ( 'NONE', #23252, .T. ) ;
#7129=EDGE_CURVE ( 'NONE', #9062, #18567, #3975, .T. ) ;
#7166=FACE_OUTER_BOUND ( 'NONE', #1633, .T. ) ;
#7173=DIRECTION ( 'NONE',  ( 1.000000000000000000, 1.000000000000000078E-15, 0.000000000000000000 ) ) ;
#7182=ORIENTED_EDGE ( 'NONE', *, *, #17103, .T. ) ;
#7204=FACE_OUTER_BOUND ( 'NONE', #16439, .T. ) ;
#7224=CARTESIAN_POINT ( 'NONE',  ( 43.31606138205700773, -21.83924545618510393, 28.60179643084731893 ) ) ;
#7230=DIRECTION ( 'NONE',  ( -1.000000000000000078E-15, 0.9439899321577417401, 0.3299742535180921199 ) ) ;
#7262=EDGE_LOOP ( 'NONE', ( #6719, #4720, #7587, #11279 ) ) ;
#7266=LINE ( 'NONE', #22974, #16580 ) ;
#7296=CARTESIAN_POINT ( 'NONE',  ( 33.31606138205700773, -12.87480755223283424, 20.78922580900563588 ) ) ;
#7307=CARTESIAN_POINT ( 'NONE',  ( 40.31606138205701484, -21.38339321089542011, 27.67811916372966863 ) ) ;
#7327=VERTEX_POINT ( 'NONE', #4241 ) ;
#7334=VECTOR ( 'NONE', #15929, 1000.000000000000227 ) ;
#7340=SURFACE_STYLE_FILL_AREA ( #20867 ) ;
#7353=CARTESIAN_POINT ( 'NONE',  ( 40.31606138205701484, -21.38339321089542011, 27.67811916372966863 ) ) ;
#7369=CARTESIAN_POINT ( 'NONE',  ( 40.31606138205700773, -19.28757846107943763, 24.56123906878952567 ) ) ;
#7401=CARTESIAN_POINT ( 'NONE',  ( 40.31606138205700773, -13.04008168869994577, 21.66778101221729713 ) ) ;
#7452=AXIS2_PLACEMENT_3D ( 'NONE', #10767, #14368, #18121 ) ;
#7476=ORIENTED_EDGE ( 'NONE', *, *, #14433, .T. ) ;
#7529=DIRECTION ( 'NONE',  ( -1.000000000000000000, -1.052872940142565459E-15, -1.848188032574765003E-17 ) ) ;
#7539=AXIS2_PLACEMENT_3D ( 'NONE', #17833, #13830, #5465 ) ;
#7540=LINE ( 'NONE', #9609, #8575 ) ;
#7551=AXIS2_PLACEMENT_3D ( 'NONE', #19602, #2326, #11892 ) ;
#7579=DIRECTION ( 'NONE',  ( 1.000000000000000000, 1.000000000000000078E-15, 0.000000000000000000 ) ) ;
#7587=ORIENTED_EDGE ( 'NONE', *, *, #1235, .T. ) ;
#7601=ORIENTED_EDGE ( 'NONE', *, *, #19451, .F. ) ;
#7687=CARTESIAN_POINT ( 'NONE',  ( 43.31606138205700773, -23.16691978223481385, 31.29201591705069063 ) ) ;
#7696=EDGE_CURVE ( 'NONE', #2503, #5245, #21851, .T. ) ;
#7705=EDGE_CURVE ( 'NONE', #12562, #16296, #72, .T. ) ;
#7757=CARTESIAN_POINT ( 'NONE',  ( 36.31606138205700773, -21.90577604921434229, 28.73660501626934760 ) ) ;
#7779=CARTESIAN_POINT ( 'NONE',  ( 38.31606138205700063, -11.98739464995938775, 18.25051608701495809 ) ) ;
#7781=MECHANICAL_DESIGN_GEOMETRIC_PRESENTATION_REPRESENTATION('',(#15978),#4086);
#7802=PLANE ( 'NONE',  #15178 ) ;
#7804=FACE_OUTER_BOUND ( 'NONE', #11944, .T. ) ;
#7861=DIRECTION ( 'NONE',  ( 1.000000000000000275E-15, -0.9439899321577401858, -0.3299742535180970604 ) ) ;
#7863=AXIS2_PLACEMENT_3D ( 'NONE', #14184, #6064, #12135 ) ;
#7869=ORIENTED_EDGE ( 'NONE', *, *, #1081, .F. ) ;
#7879=DIRECTION ( 'NONE',  ( -1.000000000000000078E-15, 0.9439899321577400748, 0.3299742535180970049 ) ) ;
#7947=ORIENTED_EDGE ( 'NONE', *, *, #5246, .F. ) ;
#7970=PLANE ( 'NONE',  #4910 ) ;
#7988=DIRECTION ( 'NONE',  ( 0.000000000000000000, 0.3299742535180963943, -0.9439899321577402969 ) ) ;
#7989=CARTESIAN_POINT ( 'NONE',  ( 40.31606138205700773, -11.51539968388051705, 18.41550321377400934 ) ) ;
#8000=VECTOR ( 'NONE', #5350, 1000.000000000000114 ) ;
#8020=CYLINDRICAL_SURFACE ( 'NONE', #14208, 0.7500000000000008882 ) ;
#8045=DIRECTION ( 'NONE',  ( 7.071067811865460542E-16, -0.4341746501209495790, -0.9008287146801832179 ) ) ;
#8060=DIRECTION ( 'NONE',  ( 1.000000000000000078E-15, -0.9439899321577417401, -0.3299742535180921199 ) ) ;
#8109=AXIS2_PLACEMENT_3D ( 'NONE', #12558, #20393, #1054 ) ;
#8149=ADVANCED_FACE ( 'NONE', ( #4646 ), #20484, .T. ) ;
#8171=ADVANCED_FACE ( 'NONE', ( #14057 ), #21910, .T. ) ;
#8188=CARTESIAN_POINT ( 'NONE',  ( 36.31606138205700773, -20.93502329652820038, 27.89939821807130826 ) ) ;
#8221=VERTEX_POINT ( 'NONE', #12643 ) ;
#8266=MANIFOLD_SOLID_BREP ( 'NONE', #2752 ) ;
#8334=CARTESIAN_POINT ( 'NONE',  ( 36.31606138205700773, -21.38339321089542722, 27.67811916372966863 ) ) ;
#8348=AXIS2_PLACEMENT_3D ( 'NONE', #2879, #3402, #5345 ) ;
#8384=CARTESIAN_POINT ( 'NONE',  ( 40.31606138205700773, -19.47805968271054766, 24.94720442500192448 ) ) ;
#8385=EDGE_CURVE ( 'NONE', #14366, #12562, #20129, .T. ) ;
#8401=CARTESIAN_POINT ( 'NONE',  ( 36.31606138205700063, -11.18542543036242343, 17.47151328161626793 ) ) ;
#8439=CARTESIAN_POINT ( 'NONE',  ( 38.31606138205700773, -22.27515649656512053, 29.48506754039017963 ) ) ;
#8443=ORIENTED_EDGE ( 'NONE', *, *, #4601, .F. ) ;
#8457=EDGE_CURVE ( 'NONE', #2232, #2532, #23167, .T. ) ;
#8470=CARTESIAN_POINT ( 'NONE',  ( 43.31606138205700063, -10.66749763588699551, 14.47455635838400134 ) ) ;
#8478=VECTOR ( 'NONE', #12775, 1000.000000000000227 ) ;
#8505=SHAPE_REPRESENTATION ( 'Upper Tension Leaf Spring', ( #2000 ), #2615 ) ;
#8523=DIRECTION ( 'NONE',  ( 0.000000000000000000, -0.3299742535180969494, 0.9439899321577399638 ) ) ;
#8527=ORIENTED_EDGE ( 'NONE', *, *, #10047, .T. ) ;
#8546=FACE_OUTER_BOUND ( 'NONE', #7262, .T. ) ;
#8556=PLANE ( 'NONE',  #20307 ) ;
#8567=ORIENTED_EDGE ( 'NONE', *, *, #9326, .F. ) ;
#8570=ORIENTED_EDGE ( 'NONE', *, *, #9504, .T. ) ;
#8573=CARTESIAN_POINT ( 'NONE',  ( 43.31606138205700773, -19.13113579875041381, 24.60350147050422720 ) ) ;
#8575=VECTOR ( 'NONE', #1845, 1000.000000000000227 ) ;
#8601=VERTEX_POINT ( 'NONE', #2538 ) ;
#8634=CIRCLE ( 'NONE', #14800, 0.7500000000000008882 ) ;
#8641=DIRECTION ( 'NONE',  ( -1.000000000000000000, -1.000000000000000078E-15, 0.000000000000000000 ) ) ;
#8656=VECTOR ( 'NONE', #19730, 1000.000000000000227 ) ;
#8674=CARTESIAN_POINT ( 'NONE',  ( 43.31606138205700063, -13.58280000135112964, 20.54174511886706256 ) ) ;
#8709=FACE_OUTER_BOUND ( 'NONE', #16050, .T. ) ;
#8769=ORIENTED_EDGE ( 'NONE', *, *, #22897, .F. ) ;
#8801=EDGE_CURVE ( 'NONE', #19706, #12956, #4931, .T. ) ;
#8817=ORIENTED_EDGE ( 'NONE', *, *, #13906, .F. ) ;
#8853=CARTESIAN_POINT ( 'NONE',  ( 43.31606138205700063, -13.25716901376041967, 21.21736665487721041 ) ) ;
#8878=CARTESIAN_POINT ( 'NONE',  ( 33.31606138205700773, -12.97731741051368459, 21.08248588348817876 ) ) ;
#8886=ORIENTED_EDGE ( 'NONE', *, *, #5242, .F. ) ;
#8901=EDGE_LOOP ( 'NONE', ( #22692, #17125, #10732, #15030 ) ) ;
#8902=FILL_AREA_STYLE_COLOUR ( '', #2411 ) ;
#8931=CARTESIAN_POINT ( 'NONE',  ( 43.31606138205700063, -12.40281258615395465, 20.95421293576468358 ) ) ;
#8941=AXIS2_PLACEMENT_3D ( 'NONE', #14106, #4324, #16150 ) ;
#8944=ADVANCED_FACE ( 'NONE', ( #15737 ), #15859, .T. ) ;
#8960=EDGE_CURVE ( 'NONE', #7089, #16232, #23588, .T. ) ;
#8982=DIRECTION ( 'NONE',  ( -1.000000000000000000, -1.000000000000000078E-15, 0.000000000000000000 ) ) ;
#8986=VERTEX_POINT ( 'NONE', #17808 ) ;
#9036=FACE_OUTER_BOUND ( 'NONE', #21597, .T. ) ;
#9037=ADVANCED_FACE ( 'NONE', ( #19217 ), #8020, .F. ) ;
#9040=VECTOR ( 'NONE', #2829, 1000.000000000000227 ) ;
#9052=FACE_OUTER_BOUND ( 'NONE', #5018, .T. ) ;
#9058=PLANE ( 'NONE',  #23853 ) ;
#9062=VERTEX_POINT ( 'NONE', #14438 ) ;
#9063=CARTESIAN_POINT ( 'NONE',  ( 36.31606138205700773, -20.71832067026706525, 29.15499406670137006 ) ) ;
#9073=ORIENTED_EDGE ( 'NONE', *, *, #7129, .F. ) ;
#9114=CARTESIAN_POINT ( 'NONE',  ( 43.31606138205700773, -19.92642959707777806, 24.72592537066031682 ) ) ;
#9121=ORIENTED_EDGE ( 'NONE', *, *, #12563, .F. ) ;
#9149=VERTEX_POINT ( 'NONE', #14561 ) ;
#9151=EDGE_CURVE ( 'NONE', #2876, #2564, #2703, .T. ) ;
#9179=PLANE ( 'NONE',  #16836 ) ;
#9223=ORIENTED_EDGE ( 'NONE', *, *, #25220, .T. ) ;
#9230=DIRECTION ( 'NONE',  ( 1.000000000000000000, 8.911169920151748851E-16, 3.114923731923493702E-16 ) ) ;
#9259=CARTESIAN_POINT ( 'NONE',  ( 38.31606138205700773, -22.27515649656512053, 29.48506754039017963 ) ) ;
#9273=PLANE ( 'NONE',  #11495 ) ;
#9286=CARTESIAN_POINT ( 'NONE',  ( 0.000000000000000000, 0.000000000000000000, 0.000000000000000000 ) ) ;
#9289=CARTESIAN_POINT ( 'NONE',  ( 36.31606138205700773, -19.13113579875042092, 24.60350147050422720 ) ) ;
#9326=EDGE_CURVE ( 'NONE', #24915, #15276, #24960, .T. ) ;
#9354=ORIENTED_EDGE ( 'NONE', *, *, #2468, .T. ) ;
#9361=CARTESIAN_POINT ( 'NONE',  ( 43.31606138205700063, -12.87480755223282358, 20.78922580900563588 ) ) ;
#9365=CARTESIAN_POINT ( 'NONE',  ( 38.31606138205700773, -22.27515649656512053, 29.48506754039017963 ) ) ;
#9400=CARTESIAN_POINT ( 'NONE',  ( 36.31606138205700063, -11.65742039644129413, 17.30652615485722023 ) ) ;
#9410=CARTESIAN_POINT ( 'NONE',  ( 43.31606138205700773, -19.92642959707777806, 24.72592537066031682 ) ) ;
#9412=CARTESIAN_POINT ( 'NONE',  ( 40.31606138205700773, -13.04008168869994577, 21.66778101221729713 ) ) ;
#9415=ADVANCED_FACE ( 'NONE', ( #9036 ), #16881, .T. ) ;
#9426=CARTESIAN_POINT ( 'NONE',  ( 33.31606138205700773, -11.53103574255889541, 17.35070425506816605 ) ) ;
#9447=CARTESIAN_POINT ( 'NONE',  ( 43.31606138205700773, -18.80550481115970740, 25.27912300651437150 ) ) ;
#9486=ORIENTED_EDGE ( 'NONE', *, *, #6302, .T. ) ;
#9504=EDGE_CURVE ( 'NONE', #1331, #16021, #13682, .T. ) ;
#9523=CARTESIAN_POINT ( 'NONE',  ( 40.31606138205700773, -12.76023008545320359, 21.53290024082827969 ) ) ;
#9524=EDGE_LOOP ( 'NONE', ( #20776, #3525, #9632, #16952, #13850, #7869, #23924, #7947, #3272, #5147, #25462 ) ) ;
#9538=CARTESIAN_POINT ( 'NONE',  ( 40.31606138205700773, -13.58280000135113319, 20.54174511886706256 ) ) ;
#9540=CARTESIAN_POINT ( 'NONE',  ( 40.31606138205700773, -11.65742039644128880, 17.30652615485722023 ) ) ;
#9542=CARTESIAN_POINT ( 'NONE',  ( 36.31606138205700773, -18.80550481115971451, 25.27912300651437150 ) ) ;
#9548=DIRECTION ( 'NONE',  ( 9.999999999999998805E-16, -0.9439899321577399638, -0.3299742535180969494 ) ) ;
#9564=VERTEX_POINT ( 'NONE', #9412 ) ;
#9599=VERTEX_POINT ( 'NONE', #13902 ) ;
#9609=CARTESIAN_POINT ( 'NONE',  ( 36.31606138205700773, -19.28757846107944474, 24.56123906878952567 ) ) ;
#9620=CIRCLE ( 'NONE', #22765, 1.250000000000000888 ) ;
#9628=VERTEX_POINT ( 'NONE', #4495 ) ;
#9632=ORIENTED_EDGE ( 'NONE', *, *, #12883, .F. ) ;
#9635=DIRECTION ( 'NONE',  ( -1.000000000000000000, -1.000000000000000078E-15, 0.000000000000000000 ) ) ;
#9659=AXIS2_PLACEMENT_3D ( 'NONE', #15630, #7529, #19617 ) ;
#9664=DIRECTION ( 'NONE',  ( 7.071067811865491110E-16, -0.9008287146801832179, 0.4341746501209495790 ) ) ;
#9690=ORIENTED_EDGE ( 'NONE', *, *, #10047, .F. ) ;
#9701=DIRECTION ( 'NONE',  ( -1.000000000000000000, -1.000000000000000078E-15, 0.000000000000000000 ) ) ;
#9714=EDGE_LOOP ( 'NONE', ( #15162, #11979, #4918, #24164 ) ) ;
#9715=LINE ( 'NONE', #4030, #15198 ) ;
#9727=EDGE_CURVE ( 'NONE', #874, #4547, #6175, .T. ) ;
#9753=EDGE_LOOP ( 'NONE', ( #12610, #22978, #23109, #19705 ) ) ;
#9763=DIRECTION ( 'NONE',  ( 9.999999999999998805E-16, -0.9439899321577399638, -0.3299742535180969494 ) ) ;
#9769=AXIS2_PLACEMENT_3D ( 'NONE', #19343, #21407, #4014 ) ;
#9777=ORIENTED_EDGE ( 'NONE', *, *, #7705, .F. ) ;
#9787=EDGE_CURVE ( 'NONE', #828, #9062, #20458, .T. ) ;
#9799=ORIENTED_EDGE ( 'NONE', *, *, #14313, .F. ) ;
#9845=CARTESIAN_POINT ( 'NONE',  ( 33.31606138205700773, -10.19550266980813724, 14.63954348514304904 ) ) ;
#9878=CARTESIAN_POINT ( 'NONE',  ( 40.31606138205701484, -20.93502329652820038, 27.89939821807130826 ) ) ;
#9886=DIRECTION ( 'NONE',  ( -9.925461516413219746E-16, 0.8967398287344630070, 0.4425581086832393041 ) ) ;
#9893=VECTOR ( 'NONE', #3906, 1000.000000000000000 ) ;
#9902=ORIENTED_EDGE ( 'NONE', *, *, #4601, .T. ) ;
#9975=LINE ( 'NONE', #9845, #21521 ) ;
#9989=VECTOR ( 'NONE', #993, 1000.000000000000227 ) ;
#9998=VECTOR ( 'NONE', #2105, 1000.000000000000000 ) ;
#9999=CARTESIAN_POINT ( 'NONE',  ( 43.31606138205700773, -21.24830114143971116, 28.89343865514767273 ) ) ;
#10004=DIRECTION ( 'NONE',  ( 4.425581086832455372E-16, -0.4425581086832455213, 0.8967398287344600094 ) ) ;
#10009=DIRECTION ( 'NONE',  ( -1.000000000000000078E-15, 0.9439899321577400748, 0.3299742535180970049 ) ) ;
#10016=ORIENTED_EDGE ( 'NONE', *, *, #25372, .T. ) ;
#10031=ORIENTED_EDGE ( 'NONE', *, *, #12418, .F. ) ;
#10047=EDGE_CURVE ( 'NONE', #9628, #9599, #23973, .T. ) ;
#10061=VERTEX_POINT ( 'NONE', #25450 ) ;
#10067=EDGE_CURVE ( 'NONE', #24915, #2564, #13493, .T. ) ;
#10085=DIRECTION ( 'NONE',  ( 0.000000000000000000, -0.3299742535180974490, 0.9439899321577398528 ) ) ;
#10103=CARTESIAN_POINT ( 'NONE',  ( 43.31606138205700773, -22.71854986786758701, 31.51329497139233737 ) ) ;
#10124=CARTESIAN_POINT ( 'NONE',  ( 36.31606138205700773, -21.45740613484710835, 28.95788407061096237 ) ) ;
#10138=DIRECTION ( 'NONE',  ( 7.071067811865460542E-16, -0.4341746501209495790, -0.9008287146801832179 ) ) ;
#10146=LINE ( 'NONE', #4351, #7334 ) ;
#10158=DIRECTION ( 'NONE',  ( 1.218693434051482139E-16, -0.4425581086832393041, 0.8967398287344630070 ) ) ;
#10245=DIRECTION ( 'NONE',  ( 1.000000000000000000, 1.000000000000000078E-15, 0.000000000000000000 ) ) ;
#10273=FACE_OUTER_BOUND ( 'NONE', #1670, .T. ) ;
#10297=FILL_AREA_STYLE ('',( #18884 ) ) ;
#10326=LINE ( 'NONE', #23836, #18410 ) ;
#10347=DIRECTION ( 'NONE',  ( 1.000000000000000000, 1.000000000000000078E-15, 0.000000000000000000 ) ) ;
#10373=LINE ( 'NONE', #8573, #22386 ) ;
#10382=CARTESIAN_POINT ( 'NONE',  ( 36.31606138205700773, -19.28757846107944474, 24.56123906878952567 ) ) ;
#10389=CARTESIAN_POINT ( 'NONE',  ( 40.31606138205700773, -19.13113579875042092, 24.60350147050422720 ) ) ;
#10481=LINE ( 'NONE', #4674, #19538 ) ;
#10496=LINE ( 'NONE', #2734, #19701 ) ;
#10509=ORIENTED_EDGE ( 'NONE', *, *, #1221, .T. ) ;
#10513=DIRECTION ( 'NONE',  ( -7.071067811865460542E-16, 0.4341746501209495790, 0.9008287146801832179 ) ) ;
#10571=CARTESIAN_POINT ( 'NONE',  ( 40.31606138205700773, -12.40281258615395821, 20.95421293576468358 ) ) ;
#10574=DIRECTION ( 'NONE',  ( 1.000000000000000000, 1.156482317317870344E-15, 0.000000000000000000 ) ) ;
#10642=DIRECTION ( 'NONE',  ( 0.000000000000000000, -0.3299742535181005021, 0.9439899321577387425 ) ) ;
#10732=ORIENTED_EDGE ( 'NONE', *, *, #15800, .T. ) ;
#10767=CARTESIAN_POINT ( 'NONE',  ( 36.31606138205700063, -11.53103574255889185, 17.35070425506816605 ) ) ;
#10769=ORIENTED_EDGE ( 'NONE', *, *, #14313, .T. ) ;
#10781=CARTESIAN_POINT ( 'NONE',  ( 33.31606138205700773, -13.25716901376043033, 21.21736665487721041 ) ) ;
#10813=EDGE_LOOP ( 'NONE', ( #21247, #3269, #20325, #12543 ) ) ;
#10820=DIRECTION ( 'NONE',  ( -1.000000000000000000, -1.052872940142565459E-15, -1.848188032574765003E-17 ) ) ;
#10823=DIRECTION ( 'NONE',  ( -1.000000000000000078E-15, 0.9439899321577400748, 0.3299742535180970049 ) ) ;
#10832=ADVANCED_FACE ( 'NONE', ( #669 ), #8556, .F. ) ;
#10896=CARTESIAN_POINT ( 'NONE',  ( 33.31606138205700773, -13.04008168869995288, 21.66778101221729713 ) ) ;
#10907=DIRECTION ( 'NONE',  ( -9.925461516413219746E-16, 0.8967398287344630070, 0.4425581086832393041 ) ) ;
#10933=VECTOR ( 'NONE', #17380, 1000.000000000000000 ) ;
#10947=ORIENTED_EDGE ( 'NONE', *, *, #19973, .T. ) ;
#10949=DIRECTION ( 'NONE',  ( 9.999999999999998805E-16, -0.9439899321577399638, -0.3299742535180969494 ) ) ;
#10956=CARTESIAN_POINT ( 'NONE',  ( 36.31606138205700063, -11.51539968388052060, 18.41550321377400934 ) ) ;
#10991=CARTESIAN_POINT ( 'NONE',  ( 36.31606138205700773, -21.38339321089542722, 27.67811916372966863 ) ) ;
#10995=LINE ( 'NONE', #5072, #3002 ) ;
#11006=CARTESIAN_POINT ( 'NONE',  ( 43.31606138205700773, -18.80550481115970740, 25.27912300651437150 ) ) ;
#11043=ORIENTED_EDGE ( 'NONE', *, *, #8385, .F. ) ;
#11045=CARTESIAN_POINT ( 'NONE',  ( 40.31606138205700773, -21.90577604921433519, 28.73660501626934050 ) ) ;
#11062=VECTOR ( 'NONE', #11912, 1000.000000000000000 ) ;
#11081=LINE ( 'NONE', #10571, #20719 ) ;
#11095=VERTEX_POINT ( 'NONE', #6307 ) ;
#11103=ORIENTED_EDGE ( 'NONE', *, *, #22533, .T. ) ;
#11111=ORIENTED_EDGE ( 'NONE', *, *, #2955, .T. ) ;
#11164=VERTEX_POINT ( 'NONE', #482 ) ;
#11215=ORIENTED_EDGE ( 'NONE', *, *, #4643, .T. ) ;
#11235=AXIS2_PLACEMENT_3D ( 'NONE', #2634, #18491, #14122 ) ;
#11251=( BOUNDED_CURVE ( )  B_SPLINE_CURVE ( 3, ( #9878, #21464, #21333, #15912 ),
 .UNSPECIFIED., .F., .T. ) 
 B_SPLINE_CURVE_WITH_KNOTS ( ( 4, 4 ),
 ( 4.712388980384689674, 6.283185307179590673 ),
 .UNSPECIFIED. ) 
 CURVE ( )  GEOMETRIC_REPRESENTATION_ITEM ( )  RATIONAL_B_SPLINE_CURVE ( ( 1.000000000000000000, 0.8047378541243649375, 0.8047378541243649375, 1.000000000000000000 ) ) 
 REPRESENTATION_ITEM ( '' )  );
#11279=ORIENTED_EDGE ( 'NONE', *, *, #16641, .T. ) ;
#11281=DIRECTION ( 'NONE',  ( -9.925461516413219746E-16, 0.8967398287344630070, 0.4425581086832393041 ) ) ;
#11285=CARTESIAN_POINT ( 'NONE',  ( 43.31606138205700773, -19.34822312381089660, 24.15308711316412627 ) ) ;
#11324=ADVANCED_FACE ( 'NONE', ( #24931 ), #4999, .T. ) ;
#11355=LINE ( 'NONE', #17270, #18499 ) ;
#11357=LINE ( 'NONE', #12570, #25075 ) ;
#11373=CARTESIAN_POINT ( 'NONE',  ( 36.31606138205700773, -21.38339321089542722, 27.67811916372966863 ) ) ;
#11394=CARTESIAN_POINT ( 'NONE',  ( 43.31606138205700773, -19.28757846107943763, 24.56123906878952567 ) ) ;
#11422=ORIENTED_EDGE ( 'NONE', *, *, #2920, .T. ) ;
#11442=CARTESIAN_POINT ( 'NONE',  ( 36.31606138205700773, -21.83924545618511104, 28.60179643084731893 ) ) ;
#11456=DIRECTION ( 'NONE',  ( 8.967398287344632705E-16, -0.8967398287344631180, -0.4425581086832391375 ) ) ;
#11475=CARTESIAN_POINT ( 'NONE',  ( 33.31606138205700773, -11.65742039644129591, 17.30652615485722023 ) ) ;
#11482=CIRCLE ( 'NONE', #21766, 3.000000000000002220 ) ;
#11489=AXIS2_PLACEMENT_3D ( 'NONE', #1414, #11600, #13526 ) ;
#11495=AXIS2_PLACEMENT_3D ( 'NONE', #9523, #3831, #19290 ) ;
#11521=EDGE_LOOP ( 'NONE', ( #25311, #8567, #24237, #13159 ) ) ;
#11531=PLANE ( 'NONE',  #7539 ) ;
#11533=CARTESIAN_POINT ( 'NONE',  ( 43.31606138205700063, -10.19550266980812658, 14.63954348514304904 ) ) ;
#11595=ORIENTED_EDGE ( 'NONE', *, *, #1881, .F. ) ;
#11600=DIRECTION ( 'NONE',  ( -1.000000000000000000, -1.000000000000000078E-15, 0.000000000000000000 ) ) ;
#11613=VECTOR ( 'NONE', #19924, 1000.000000000000227 ) ;
#11616=VECTOR ( 'NONE', #10158, 1000.000000000000227 ) ;
#11638=EDGE_CURVE ( 'NONE', #2876, #828, #2517, .T. ) ;
#11653=DIRECTION ( 'NONE',  ( 1.000000000000000000, 8.673617379884027583E-16, 0.000000000000000000 ) ) ;
#11657=ORIENTED_EDGE ( 'NONE', *, *, #12651, .T. ) ;
#11684=AXIS2_PLACEMENT_3D ( 'NONE', #7369, #25111, #3744 ) ;
#11722=VERTEX_POINT ( 'NONE', #18377 ) ;
#11750=ORIENTED_EDGE ( 'NONE', *, *, #13822, .T. ) ;
#11767=FACE_OUTER_BOUND ( 'NONE', #18830, .T. ) ;
#11771=CARTESIAN_POINT ( 'NONE',  ( 40.31606138205701484, -22.71854986786759056, 31.51329497139233737 ) ) ;
#11780=DIRECTION ( 'NONE',  ( 1.000000000000000275E-15, -0.9439899321577401858, -0.3299742535180970604 ) ) ;
#11860=ADVANCED_FACE ( 'NONE', ( #7166 ), #5228, .T. ) ;
#11888=DIRECTION ( 'NONE',  ( -7.071067811865491110E-16, 0.9008287146801832179, -0.4341746501209495790 ) ) ;
#11890=LINE ( 'NONE', #16110, #8656 ) ;
#11892=DIRECTION ( 'NONE',  ( 0.000000000000000000, -0.3299742535180974490, 0.9439899321577398528 ) ) ;
#11912=DIRECTION ( 'NONE',  ( -1.000000000000000000, -1.000000000000000078E-15, 0.000000000000000000 ) ) ;
#11944=EDGE_LOOP ( 'NONE', ( #3334, #17861, #3054, #16445 ) ) ;
#11979=ORIENTED_EDGE ( 'NONE', *, *, #23552, .T. ) ;
#12017=DIRECTION ( 'NONE',  ( 0.000000000000000000, 0.3299742535180963943, -0.9439899321577402969 ) ) ;
#12022=DIRECTION ( 'NONE',  ( -1.000000000000000000, -1.000000000000000078E-15, 0.000000000000000000 ) ) ;
#12042=CARTESIAN_POINT ( 'NONE',  ( 36.31606138205700063, -13.04008168869994932, 21.66778101221729713 ) ) ;
#12055=CARTESIAN_POINT ( 'NONE',  ( 36.31606138205700063, -11.51539968388052060, 18.41550321377400934 ) ) ;
#12061=VERTEX_POINT ( 'NONE', #1718 ) ;
#12063=ORIENTED_EDGE ( 'NONE', *, *, #20664, .T. ) ;
#12093=EDGE_CURVE ( 'NONE', #2564, #24591, #3418, .T. ) ;
#12135=DIRECTION ( 'NONE',  ( 0.000000000000000000, -0.3299742535180970049, 0.9439899321577400748 ) ) ;
#12156=PLANE ( 'NONE',  #13975 ) ;
#12167=ORIENTED_EDGE ( 'NONE', *, *, #799, .F. ) ;
#12176=EDGE_CURVE ( 'NONE', #16232, #11095, #16272, .T. ) ;
#12187=LINE ( 'NONE', #20156, #4413 ) ;
#12206=ORIENTED_EDGE ( 'NONE', *, *, #12651, .F. ) ;
#12235=SURFACE_SIDE_STYLE ('',( #16082 ) ) ;
#12255=ORIENTED_EDGE ( 'NONE', *, *, #21384, .F. ) ;
#12272=CARTESIAN_POINT ( 'NONE',  ( 43.31606138205700063, -12.40281258615395465, 20.95421293576468358 ) ) ;
#12273=( BOUNDED_CURVE ( )  B_SPLINE_CURVE ( 3, ( #9365, #17214, #25035, #8334 ),
 .UNSPECIFIED., .F., .T. ) 
 B_SPLINE_CURVE_WITH_KNOTS ( ( 4, 4 ),
 ( 0.000000000000000000, 1.570796326794895004 ),
 .UNSPECIFIED. ) 
 CURVE ( )  GEOMETRIC_REPRESENTATION_ITEM ( )  RATIONAL_B_SPLINE_CURVE ( ( 1.000000000000000000, 0.8047378541243649375, 0.8047378541243649375, 1.000000000000000000 ) ) 
 REPRESENTATION_ITEM ( '' )  );
#12295=DIRECTION ( 'NONE',  ( 0.000000000000000000, 0.4425581086832394706, -0.8967398287344628960 ) ) ;
#12310=LINE ( 'NONE', #8439, #24142 ) ;
#12352=CARTESIAN_POINT ( 'NONE',  ( 43.31606138205700773, -19.73594837544666802, 24.33996001444790025 ) ) ;
#12397=AXIS2_PLACEMENT_3D ( 'NONE', #6001, #10245, #2247 ) ;
#12412=DIRECTION ( 'NONE',  ( 0.000000000000000000, -0.3299742535180969494, 0.9439899321577399638 ) ) ;
#12418=EDGE_CURVE ( 'NONE', #2564, #3312, #10995, .T. ) ;
#12475=VECTOR ( 'NONE', #17467, 1000.000000000000000 ) ;
#12478=VECTOR ( 'NONE', #6512, 1000.000000000000000 ) ;
#12517=FACE_OUTER_BOUND ( 'NONE', #1490, .T. ) ;
#12543=ORIENTED_EDGE ( 'NONE', *, *, #20502, .T. ) ;
#12552=AXIS2_PLACEMENT_3D ( 'NONE', #21063, #9230, #5220 ) ;
#12558=CARTESIAN_POINT ( 'NONE',  ( 43.31606138205700773, -18.80550481115970740, 25.27912300651437150 ) ) ;
#12561=DIRECTION ( 'NONE',  ( 1.000000000000000275E-15, -0.9439899321577400748, -0.3299742535180970049 ) ) ;
#12562=VERTEX_POINT ( 'NONE', #754 ) ;
#12563=EDGE_CURVE ( 'NONE', #1030, #11095, #13725, .T. ) ;
#12568=ADVANCED_FACE ( 'NONE', ( #11767 ), #17682, .T. ) ;
#12569=CARTESIAN_POINT ( 'NONE',  ( 40.31606138205700773, -10.66749763588699906, 14.47455635838400134 ) ) ;
#12570=CARTESIAN_POINT ( 'NONE',  ( 43.31606138205700773, -19.34822312381089660, 24.15308711316412627 ) ) ;
#12610=ORIENTED_EDGE ( 'NONE', *, *, #13971, .T. ) ;
#12611=ORIENTED_EDGE ( 'NONE', *, *, #9326, .T. ) ;
#12616=EDGE_CURVE ( 'NONE', #17216, #2232, #9620, .T. ) ;
#12627=VERTEX_POINT ( 'NONE', #12272 ) ;
#12632=FACE_OUTER_BOUND ( 'NONE', #18926, .T. ) ;
#12635=CARTESIAN_POINT ( 'NONE',  ( 33.31606138205700773, -12.87480755223283424, 20.78922580900563588 ) ) ;
#12641=AXIS2_PLACEMENT_3D ( 'NONE', #10896, #13217, #1213 ) ;
#12643=CARTESIAN_POINT ( 'NONE',  ( 43.31606138205700773, -19.47805968271054766, 24.94720442500192448 ) ) ;
#12651=EDGE_CURVE ( 'NONE', #546, #9564, #18651, .T. ) ;
#12671=CARTESIAN_POINT ( 'NONE',  ( 43.31606138205700773, -19.92642959707777806, 24.72592537066031682 ) ) ;
#12708=CARTESIAN_POINT ( 'NONE',  ( 43.31606138205700063, -10.66749763588699551, 14.47455635838400134 ) ) ;
#12765=DIRECTION ( 'NONE',  ( 0.000000000000000000, 0.3299742535180974490, -0.9439899321577398528 ) ) ;
#12766=DIRECTION ( 'NONE',  ( 0.000000000000000000, 0.000000000000000000, 1.000000000000000000 ) ) ;
#12775=DIRECTION ( 'NONE',  ( 0.000000000000000000, 0.3299742535180969494, -0.9439899321577399638 ) ) ;
#12814=DIRECTION ( 'NONE',  ( -1.000000000000000000, -1.052872940142565459E-15, -1.848188032574765003E-17 ) ) ;
#12834=ORIENTED_EDGE ( 'NONE', *, *, #5900, .T. ) ;
#12836=VERTEX_POINT ( 'NONE', #22170 ) ;
#12844=CARTESIAN_POINT ( 'NONE',  ( 43.31606138205700063, -10.19550266980812658, 14.63954348514304904 ) ) ;
#12852=ORIENTED_EDGE ( 'NONE', *, *, #23409, .F. ) ;
#12854=EDGE_CURVE ( 'NONE', #874, #546, #639, .T. ) ;
#12883=EDGE_CURVE ( 'NONE', #3532, #19706, #6966, .T. ) ;
#12888=DIRECTION ( 'NONE',  ( -1.000000000000000078E-15, 0.9439899321577400748, 0.3299742535180970049 ) ) ;
#12917=ORIENTED_EDGE ( 'NONE', *, *, #17904, .T. ) ;
#12933=CARTESIAN_POINT ( 'NONE',  ( 43.31606138205700063, -10.19550266980812658, 14.63954348514304904 ) ) ;
#12937=DIRECTION ( 'NONE',  ( 0.000000000000000000, 0.3299742535180969494, -0.9439899321577399638 ) ) ;
#12939=CARTESIAN_POINT ( 'NONE',  ( 36.31606138205700773, -21.39087554181787354, 28.82307548518891238 ) ) ;
#12956=VERTEX_POINT ( 'NONE', #15070 ) ;
#12998=CARTESIAN_POINT ( 'NONE',  ( 33.31606138205700773, -19.92642959707779227, 24.72592537066031682 ) ) ;
#13019=DIRECTION ( 'NONE',  ( 1.000000000000000000, 8.911169920151748851E-16, 3.114923731923493702E-16 ) ) ;
#13035=VERTEX_POINT ( 'NONE', #7224 ) ;
#13058=VECTOR ( 'NONE', #11888, 1000.000000000000227 ) ;
#13069=ORIENTED_EDGE ( 'NONE', *, *, #21377, .T. ) ;
#13087=EDGE_LOOP ( 'NONE', ( #20546, #23661, #659, #22811 ) ) ;
#13091=SHAPE_REPRESENTATION_RELATIONSHIP ( 'NONE' , 'NONE' ,  #8505, #20587 ) ;
#13131=DIRECTION ( 'NONE',  ( 1.000000000000000275E-15, -0.9439899321577401858, -0.3299742535180970604 ) ) ;
#13142=LINE ( 'NONE', #9289, #5516 ) ;
#13158=DIRECTION ( 'NONE',  ( 1.218693434051482139E-16, -0.4425581086832393041, 0.8967398287344630070 ) ) ;
#13159=ORIENTED_EDGE ( 'NONE', *, *, #12418, .T. ) ;
#13163=DIRECTION ( 'NONE',  ( 1.000000000000000000, 1.000000000000000078E-15, 0.000000000000000000 ) ) ;
#13181=AXIS2_PLACEMENT_3D ( 'NONE', #7779, #2087, #13573 ) ;
#13217=DIRECTION ( 'NONE',  ( -1.000000000000000000, -1.052872940142565459E-15, -1.848188032574765003E-17 ) ) ;
#13255=AXIS2_PLACEMENT_3D ( 'NONE', #9400, #23157, #13394 ) ;
#13303=DIRECTION ( 'NONE',  ( 0.000000000000000000, 0.3299742535180974490, -0.9439899321577398528 ) ) ;
#13328=CARTESIAN_POINT ( 'NONE',  ( 40.31606138205700773, -11.98739464995938597, 18.25051608701495809 ) ) ;
#13394=DIRECTION ( 'NONE',  ( 1.000000000000000000, 1.156482317317870344E-15, 0.000000000000000000 ) ) ;
#13423=CARTESIAN_POINT ( 'NONE',  ( 43.31606138205700063, -11.65742039644128702, 17.30652615485722023 ) ) ;
#13452=LINE ( 'NONE', #11285, #21746 ) ;
#13476=VECTOR ( 'NONE', #16903, 1000.000000000000227 ) ;
#13477=LINE ( 'NONE', #9999, #15529 ) ;
#13493=LINE ( 'NONE', #21344, #19051 ) ;
#13519=EDGE_CURVE ( 'NONE', #5254, #17216, #10373, .T. ) ;
#13526=DIRECTION ( 'NONE',  ( 0.000000000000000000, -0.3299742535180974490, 0.9439899321577398528 ) ) ;
#13527=DIRECTION ( 'NONE',  ( 1.218693434051482139E-16, -0.4425581086832393041, 0.8967398287344630070 ) ) ;
#13551=CARTESIAN_POINT ( 'NONE',  ( 36.31606138205700773, -21.45740613484710479, 28.95788407061096237 ) ) ;
#13573=DIRECTION ( 'NONE',  ( 1.000000000000000000, 8.673617379884027583E-16, 0.000000000000000000 ) ) ;
#13619=VECTOR ( 'NONE', #15845, 1000.000000000000227 ) ;
#13634=CARTESIAN_POINT ( 'NONE',  ( 43.31606138205700773, -19.28757846107943763, 24.56123906878952567 ) ) ;
#13640=DIRECTION ( 'NONE',  ( 7.071067811865491110E-16, -0.9008287146801832179, 0.4341746501209495790 ) ) ;
#13647=DIRECTION ( 'NONE',  ( 1.000000000000000000, 1.000000000000000078E-15, 0.000000000000000000 ) ) ;
#13682=CIRCLE ( 'NONE', #23540, 3.000000000000002665 ) ;
#13690=CARTESIAN_POINT ( 'NONE',  ( 40.31606138205701484, -23.16691978223481385, 31.29201591705069063 ) ) ;
#13725=CIRCLE ( 'NONE', #7551, 1.250000000000000888 ) ;
#13726=FACE_OUTER_BOUND ( 'NONE', #16691, .T. ) ;
#13745=ORIENTED_EDGE ( 'NONE', *, *, #15190, .T. ) ;
#13746=DIRECTION ( 'NONE',  ( -1.000000000000000000, -1.052872940142565459E-15, -1.848188032574765003E-17 ) ) ;
#13758=CARTESIAN_POINT ( 'NONE',  ( 33.31606138205700773, -19.13113579875042802, 24.60350147050422720 ) ) ;
#13780=ADVANCED_FACE ( 'NONE', ( #7010 ), #14996, .F. ) ;
#13795=CARTESIAN_POINT ( 'NONE',  ( 36.31606138205700063, -13.58280000135113674, 20.54174511886706256 ) ) ;
#13812=DIRECTION ( 'NONE',  ( 1.000000000000000000, 8.911169920151748851E-16, 3.114923731923493702E-16 ) ) ;
#13822=EDGE_CURVE ( 'NONE', #8986, #17509, #7266, .T. ) ;
#13830=DIRECTION ( 'NONE',  ( -1.000000000000000000, -1.052872940142565459E-15, -1.848188032574765003E-17 ) ) ;
#13850=ORIENTED_EDGE ( 'NONE', *, *, #4846, .F. ) ;
#13865=PLANE ( 'NONE',  #454 ) ;
#13875=( BOUNDED_SURFACE ( )  B_SPLINE_SURFACE ( 3, 1, ( 
 ( #17721, #52 ),
 ( #20282, #1422 ),
 ( #18594, #6619 ),
 ( #22206, #7353 ) ),
 .UNSPECIFIED., .F., .F., .T. ) 
 B_SPLINE_SURFACE_WITH_KNOTS ( ( 4, 4 ),
 ( 2, 2 ),
 ( 0.000000000000000000, 1.000000000000000000 ),
 ( 0.000000000000000000, 1.000000000000000000 ),
 .UNSPECIFIED. ) 
 GEOMETRIC_REPRESENTATION_ITEM ( )  RATIONAL_B_SPLINE_SURFACE ( (
 ( 1.000000000000000000, 1.000000000000000000),
 ( 0.8047378541243649375, 0.8047378541243649375),
 ( 0.8047378541243649375, 0.8047378541243649375),
 ( 1.000000000000000000, 1.000000000000000000) ) ) 
 REPRESENTATION_ITEM ( '' )  SURFACE ( )  );
#13902=CARTESIAN_POINT ( 'NONE',  ( 43.31606138205700063, -13.25716901376041967, 21.21736665487721041 ) ) ;
#13905=( LENGTH_UNIT ( ) NAMED_UNIT ( * ) SI_UNIT ( .MILLI., .METRE. ) );
#13906=EDGE_CURVE ( 'NONE', #9564, #12562, #23611, .T. ) ;
#13931=VECTOR ( 'NONE', #22856, 1000.000000000000227 ) ;
#13938=CARTESIAN_POINT ( 'NONE',  ( 36.31606138205700063, -13.25716901376042856, 21.21736665487721041 ) ) ;
#13971=EDGE_CURVE ( 'NONE', #8221, #18554, #1833, .T. ) ;
#13975=AXIS2_PLACEMENT_3D ( 'NONE', #15746, #13812, #18069 ) ;
#13990=VECTOR ( 'NONE', #9548, 1000.000000000000227 ) ;
#14005=ORIENTED_EDGE ( 'NONE', *, *, #2958, .F. ) ;
#14011=ADVANCED_FACE ( 'NONE', ( #19235 ), #1573, .T. ) ;
#14018=ORIENTED_EDGE ( 'NONE', *, *, #4765, .T. ) ;
#14024=LINE ( 'NONE', #3972, #4608 ) ;
#14040=EDGE_LOOP ( 'NONE', ( #22994, #5360, #6035, #899 ) ) ;
#14057=FACE_OUTER_BOUND ( 'NONE', #14329, .T. ) ;
#14067=( BOUNDED_CURVE ( )  B_SPLINE_CURVE ( 3, ( #2250, #309, #10124, #8188 ),
 .UNSPECIFIED., .F., .T. ) 
 B_SPLINE_CURVE_WITH_KNOTS ( ( 4, 4 ),
 ( 0.000000000000000000, 1.570796326794895004 ),
 .UNSPECIFIED. ) 
 CURVE ( )  GEOMETRIC_REPRESENTATION_ITEM ( )  RATIONAL_B_SPLINE_CURVE ( ( 1.000000000000000000, 0.8047378541243649375, 0.8047378541243649375, 1.000000000000000000 ) ) 
 REPRESENTATION_ITEM ( '' )  );
#14080=LINE ( 'NONE', #23978, #5361 ) ;
#14086=DIRECTION ( 'NONE',  ( -1.000000000000000000, -1.000000000000000078E-15, 0.000000000000000000 ) ) ;
#14091=AXIS2_PLACEMENT_3D ( 'NONE', #15040, #23020, #2798 ) ;
#14106=CARTESIAN_POINT ( 'NONE',  ( 40.31606138205700773, -18.80550481115971095, 25.27912300651437150 ) ) ;
#14109=ORIENTED_EDGE ( 'NONE', *, *, #13519, .T. ) ;
#14122=DIRECTION ( 'NONE',  ( 0.000000000000000000, 0.4425581086832400257, -0.8967398287344627850 ) ) ;
#14164=DIRECTION ( 'NONE',  ( 9.999999999999998805E-16, -0.9439899321577399638, -0.3299742535180969494 ) ) ;
#14184=CARTESIAN_POINT ( 'NONE',  ( 36.31606138205700063, -13.58280000135113674, 20.54174511886706256 ) ) ;
#14186=ORIENTED_EDGE ( 'NONE', *, *, #20104, .T. ) ;
#14208=AXIS2_PLACEMENT_3D ( 'NONE', #9447, #9701, #17420 ) ;
#14233=CARTESIAN_POINT ( 'NONE',  ( 38.31606138205700773, -21.82678658219787948, 29.70634659473178019 ) ) ;
#14248=ADVANCED_FACE ( 'NONE', ( #20991 ), #4669, .F. ) ;
#14292=FACE_OUTER_BOUND ( 'NONE', #23367, .T. ) ;
#14294=ORIENTED_EDGE ( 'NONE', *, *, #21384, .T. ) ;
#14313=EDGE_CURVE ( 'NONE', #3261, #1701, #23516, .T. ) ;
#14329=EDGE_LOOP ( 'NONE', ( #21751, #5492, #12852, #20685 ) ) ;
#14333=ORIENTED_EDGE ( 'NONE', *, *, #15397, .T. ) ;
#14366=VERTEX_POINT ( 'NONE', #23796 ) ;
#14368=DIRECTION ( 'NONE',  ( 1.000000000000000275E-15, -0.9439899321577401858, -0.3299742535180970604 ) ) ;
#14409=AXIS2_PLACEMENT_3D ( 'NONE', #760, #4397, #22416 ) ;
#14417=AXIS2_PLACEMENT_3D ( 'NONE', #19457, #1799, #7879 ) ;
#14418=DIRECTION ( 'NONE',  ( 1.000000000000000000, 1.000000000000000078E-15, 0.000000000000000000 ) ) ;
#14422=AXIS2_PLACEMENT_3D ( 'NONE', #13634, #11456, #21489 ) ;
#14433=EDGE_CURVE ( 'NONE', #17509, #12956, #19559, .T. ) ;
#14434=EDGE_CURVE ( 'NONE', #11095, #18567, #19422, .T. ) ;
#14438=CARTESIAN_POINT ( 'NONE',  ( 33.31606138205700773, -19.34822312381090370, 24.15308711316412627 ) ) ;
#14441=CIRCLE ( 'NONE', #12397, 0.7499999999999997780 ) ;
#14464=EDGE_CURVE ( 'NONE', #9599, #17216, #14024, .T. ) ;
#14472=CARTESIAN_POINT ( 'NONE',  ( 43.31606138205700063, -13.25716901376041967, 21.21736665487721041 ) ) ;
#14494=CARTESIAN_POINT ( 'NONE',  ( 40.31606138205701484, -23.16691978223481385, 31.29201591705069063 ) ) ;
#14500=CIRCLE ( 'NONE', #11235, 2.999999999999998668 ) ;
#14557=ORIENTED_EDGE ( 'NONE', *, *, #5900, .F. ) ;
#14561=CARTESIAN_POINT ( 'NONE',  ( 36.31606138205700063, -10.19550266980813369, 14.63954348514304904 ) ) ;
#14575=ORIENTED_EDGE ( 'NONE', *, *, #16496, .T. ) ;
#14578=CARTESIAN_POINT ( 'NONE',  ( 43.31606138205700063, -12.97731741051367393, 21.08248588348817876 ) ) ;
#14627=ORIENTED_EDGE ( 'NONE', *, *, #16641, .F. ) ;
#14748=CARTESIAN_POINT ( 'NONE',  ( 40.31606138205700773, -10.66749763588699906, 14.47455635838400134 ) ) ;
#14764=LINE ( 'NONE', #20564, #5744 ) ;
#14768=ORIENTED_EDGE ( 'NONE', *, *, #4846, .T. ) ;
#14770=CARTESIAN_POINT ( 'NONE',  ( 36.31606138205700063, -12.97731741051368282, 21.08248588348817876 ) ) ;
#14800=AXIS2_PLACEMENT_3D ( 'NONE', #1460, #14858, #20800 ) ;
#14807=PLANE ( 'NONE',  #17425 ) ;
#14858=DIRECTION ( 'NONE',  ( 1.000000000000000000, 1.000000000000000078E-15, 0.000000000000000000 ) ) ;
#14869=LINE ( 'NONE', #3528, #8000 ) ;
#14892=DIRECTION ( 'NONE',  ( -7.071067811865491110E-16, 0.9008287146801832179, -0.4341746501209495790 ) ) ;
#14916=EDGE_CURVE ( 'NONE', #11164, #11722, #21767, .T. ) ;
#14963=FACE_OUTER_BOUND ( 'NONE', #21368, .T. ) ;
#14996=CYLINDRICAL_SURFACE ( 'NONE', #24787, 0.7500000000000008882 ) ;
#15030=ORIENTED_EDGE ( 'NONE', *, *, #3276, .F. ) ;
#15040=CARTESIAN_POINT ( 'NONE',  ( 43.31606138205700773, -19.73594837544666802, 24.33996001444790025 ) ) ;
#15053=AXIS2_PLACEMENT_3D ( 'NONE', #6204, #4148, #12017 ) ;
#15070=CARTESIAN_POINT ( 'NONE',  ( 33.31606138205700773, -21.39087554181787354, 28.82307548518891238 ) ) ;
#15098=EDGE_CURVE ( 'NONE', #13035, #15148, #14500, .T. ) ;
#15144=EDGE_LOOP ( 'NONE', ( #9073, #169, #7601, #2382 ) ) ;
#15148=VERTEX_POINT ( 'NONE', #14494 ) ;
#15162=ORIENTED_EDGE ( 'NONE', *, *, #15397, .F. ) ;
#15178=AXIS2_PLACEMENT_3D ( 'NONE', #18104, #15648, #19769 ) ;
#15181=ORIENTED_EDGE ( 'NONE', *, *, #24809, .T. ) ;
#15187=PRESENTATION_STYLE_ASSIGNMENT (( #24842 ) ) ;
#15190=EDGE_CURVE ( 'NONE', #12627, #546, #16288, .T. ) ;
#15198=VECTOR ( 'NONE', #17566, 1000.000000000000227 ) ;
#15249=ADVANCED_FACE ( 'NONE', ( #3010 ), #22980, .F. ) ;
#15253=FACE_OUTER_BOUND ( 'NONE', #827, .T. ) ;
#15276=VERTEX_POINT ( 'NONE', #18608 ) ;
#15337=VECTOR ( 'NONE', #24478, 1000.000000000000000 ) ;
#15346=CYLINDRICAL_SURFACE ( 'NONE', #19473, 1.250000000000000888 ) ;
#15349=CARTESIAN_POINT ( 'NONE',  ( 38.31606138205700773, -22.27515649656512053, 29.48506754039017963 ) ) ;
#15374=ORIENTED_EDGE ( 'NONE', *, *, #17933, .F. ) ;
#15397=EDGE_CURVE ( 'NONE', #30, #1030, #9975, .T. ) ;
#15401=VECTOR ( 'NONE', #8045, 1000.000000000000227 ) ;
#15405=ORIENTED_EDGE ( 'NONE', *, *, #2468, .F. ) ;
#15406=ADVANCED_FACE ( 'NONE', ( #15253 ), #11531, .T. ) ;
#15424=CARTESIAN_POINT ( 'NONE',  ( 43.31606138205700063, -13.58280000135112964, 20.54174511886706256 ) ) ;
#15433=FACE_OUTER_BOUND ( 'NONE', #18128, .T. ) ;
#15471=DIRECTION ( 'NONE',  ( -1.000000000000000000, -1.000000000000000078E-15, 0.000000000000000000 ) ) ;
#15478=ORIENTED_EDGE ( 'NONE', *, *, #21408, .F. ) ;
#15498=PLANE ( 'NONE',  #5901 ) ;
#15529=VECTOR ( 'NONE', #3548, 1000.000000000000114 ) ;
#15544=ADVANCED_FACE ( 'NONE', ( #25277 ), #15498, .T. ) ;
#15551=FACE_OUTER_BOUND ( 'NONE', #4540, .T. ) ;
#15565=DIRECTION ( 'NONE',  ( 7.071067811865460542E-16, -0.4341746501209495790, -0.9008287146801832179 ) ) ;
#15579=EDGE_LOOP ( 'NONE', ( #14294, #5742, #11595, #16597 ) ) ;
#15589=ORIENTED_EDGE ( 'NONE', *, *, #24809, .F. ) ;
#15594=EDGE_LOOP ( 'NONE', ( #8886, #12255, #10509, #6448 ) ) ;
#15612=EDGE_CURVE ( 'NONE', #20448, #10061, #6229, .T. ) ;
#15630=CARTESIAN_POINT ( 'NONE',  ( 40.31606138205700773, -18.80550481115971095, 25.27912300651437150 ) ) ;
#15648=DIRECTION ( 'NONE',  ( -1.000000000000000000, -1.052872940142565459E-15, -1.848188032574765003E-17 ) ) ;
#15651=DIRECTION ( 'NONE',  ( 1.000000000000000000, 1.000000000000000078E-15, 0.000000000000000000 ) ) ;
#15688=CIRCLE ( 'NONE', #4594, 0.7500000000000021094 ) ;
#15719=ADVANCED_FACE ( 'NONE', ( #8546 ), #20388, .T. ) ;
#15737=FACE_OUTER_BOUND ( 'NONE', #14040, .T. ) ;
#15744=DIRECTION ( 'NONE',  ( -1.000000000000000000, -1.000000000000000078E-15, 0.000000000000000000 ) ) ;
#15746=CARTESIAN_POINT ( 'NONE',  ( 43.31606138205700773, -19.13113579875041381, 24.60350147050422720 ) ) ;
#15757=ORIENTED_EDGE ( 'NONE', *, *, #1235, .F. ) ;
#15760=CARTESIAN_POINT ( 'NONE',  ( 36.31606138205700773, -18.80550481115971451, 25.27912300651437150 ) ) ;
#15762=VECTOR ( 'NONE', #17445, 1000.000000000000227 ) ;
#15781=EDGE_LOOP ( 'NONE', ( #4708, #15589, #11111, #17857 ) ) ;
#15800=EDGE_CURVE ( 'NONE', #12061, #3532, #22827, .T. ) ;
#15808=CARTESIAN_POINT ( 'NONE',  ( 43.31606138205700773, -21.39087554181786643, 28.82307548518891238 ) ) ;
#15822=CARTESIAN_POINT ( 'NONE',  ( 33.31606138205700773, -12.76023008545321069, 21.53290024082827969 ) ) ;
#15845=DIRECTION ( 'NONE',  ( 9.925461516413219746E-16, -0.8967398287344630070, -0.4425581086832393041 ) ) ;
#15859=CYLINDRICAL_SURFACE ( 'NONE', #9769, 3.000000000000000444 ) ;
#15861=CARTESIAN_POINT ( 'NONE',  ( 33.31606138205700773, -10.66749763588700617, 14.47455635838400134 ) ) ;
#15868=FACE_OUTER_BOUND ( 'NONE', #9753, .T. ) ;
#15911=ORIENTED_EDGE ( 'NONE', *, *, #25288, .T. ) ;
#15912=CARTESIAN_POINT ( 'NONE',  ( 38.31606138205700773, -21.82678658219787948, 29.70634659473178019 ) ) ;
#15929=DIRECTION ( 'NONE',  ( 9.925461516413219746E-16, -0.8967398287344630070, -0.4425581086832393041 ) ) ;
#15960=ORIENTED_EDGE ( 'NONE', *, *, #4479, .F. ) ;
#15978=STYLED_ITEM ( 'NONE', ( #15187 ), #8266 ) ;
#16016=LINE ( 'NONE', #14472, #18013 ) ;
#16019=ADVANCED_FACE ( 'NONE', ( #21402 ), #5564, .F. ) ;
#16021=VERTEX_POINT ( 'NONE', #13423 ) ;
#16026=ADVANCED_FACE ( 'NONE', ( #21533 ), #15346, .T. ) ;
#16029=DIRECTION ( 'NONE',  ( 9.925461516413219746E-16, -0.8967398287344630070, -0.4425581086832393041 ) ) ;
#16045=FACE_OUTER_BOUND ( 'NONE', #4293, .T. ) ;
#16050=EDGE_LOOP ( 'NONE', ( #568, #14627, #9799, #23259 ) ) ;
#16082=SURFACE_STYLE_FILL_AREA ( #10297 ) ;
#16110=CARTESIAN_POINT ( 'NONE',  ( 36.31606138205700773, -19.47805968271055477, 24.94720442500192448 ) ) ;
#16132=CARTESIAN_POINT ( 'NONE',  ( 43.31606138205700063, -10.19550266980812658, 14.63954348514304904 ) ) ;
#16150=DIRECTION ( 'NONE',  ( 0.000000000000000000, -0.3299742535181005021, 0.9439899321577387425 ) ) ;
#16190=DIRECTION ( 'NONE',  ( 0.000000000000000000, -0.3299742535180970049, 0.9439899321577400748 ) ) ;
#16228=ORIENTED_EDGE ( 'NONE', *, *, #22533, .F. ) ;
#16232=VERTEX_POINT ( 'NONE', #18310 ) ;
#16241=DIRECTION ( 'NONE',  ( 1.000000000000000000, 1.156482317317870344E-15, 0.000000000000000000 ) ) ;
#16272=LINE ( 'NONE', #23870, #9998 ) ;
#16288=LINE ( 'NONE', #24136, #12478 ) ;
#16293=ADVANCED_FACE ( 'NONE', ( #20358 ), #14807, .F. ) ;
#16296=VERTEX_POINT ( 'NONE', #18678 ) ;
#16312=EDGE_CURVE ( 'NONE', #546, #14366, #11081, .T. ) ;
#16397=DIRECTION ( 'NONE',  ( 0.000000000000000000, 0.4425581086832394706, -0.8967398287344628960 ) ) ;
#16439=EDGE_LOOP ( 'NONE', ( #16566, #15960, #10947, #22268 ) ) ;
#16445=ORIENTED_EDGE ( 'NONE', *, *, #22923, .F. ) ;
#16479=CARTESIAN_POINT ( 'NONE',  ( 40.31606138205700773, -11.18542543036241987, 17.47151328161626793 ) ) ;
#16484=AXIS2_PLACEMENT_3D ( 'NONE', #22662, #16734, #6821 ) ;
#16496=EDGE_CURVE ( 'NONE', #7089, #126, #13142, .T. ) ;
#16525=DIRECTION ( 'NONE',  ( 0.000000000000000000, -0.3299742535180969494, 0.9439899321577399638 ) ) ;
#16527=CARTESIAN_POINT ( 'NONE',  ( 40.31606138205700773, -19.47805968271054766, 24.94720442500192448 ) ) ;
#16555=VECTOR ( 'NONE', #14164, 1000.000000000000227 ) ;
#16560=AXIS2_PLACEMENT_3D ( 'NONE', #8853, #22367, #4842 ) ;
#16566=ORIENTED_EDGE ( 'NONE', *, *, #9727, .F. ) ;
#16574=AXIS2_PLACEMENT_3D ( 'NONE', #15424, #7579, #1621 ) ;
#16580=VECTOR ( 'NONE', #5338, 1000.000000000000000 ) ;
#16597=ORIENTED_EDGE ( 'NONE', *, *, #22897, .T. ) ;
#16599=VECTOR ( 'NONE', #8523, 1000.000000000000227 ) ;
#16631=PRODUCT_DEFINITION_FORMATION_WITH_SPECIFIED_SOURCE ( 'ANY', '', #1662, .NOT_KNOWN. ) ;
#16641=EDGE_CURVE ( 'NONE', #1701, #9149, #20997, .T. ) ;
#16665=CARTESIAN_POINT ( 'NONE',  ( 33.31606138205700773, -19.47805968271055477, 24.94720442500192448 ) ) ;
#16670=ORIENTED_EDGE ( 'NONE', *, *, #25440, .T. ) ;
#16691=EDGE_LOOP ( 'NONE', ( #18994, #24472, #14557, #20479 ) ) ;
#16703=CARTESIAN_POINT ( 'NONE',  ( 43.31606138205700063, -12.76023008545320181, 21.53290024082827969 ) ) ;
#16705=APPLICATION_CONTEXT ( 'automotive_design' ) ;
#16724=ORIENTED_EDGE ( 'NONE', *, *, #19451, .T. ) ;
#16734=DIRECTION ( 'NONE',  ( 1.000000000000000000, 8.911169920151748851E-16, 3.114923731923493702E-16 ) ) ;
#16744=AXIS2_PLACEMENT_3D ( 'NONE', #8931, #18462, #16775 ) ;
#16766=LINE ( 'NONE', #1168, #13476 ) ;
#16775=DIRECTION ( 'NONE',  ( 0.000000000000000000, -0.3299742535180970049, 0.9439899321577400748 ) ) ;
#16792=EDGE_CURVE ( 'NONE', #10061, #8601, #14869, .T. ) ;
#16836=AXIS2_PLACEMENT_3D ( 'NONE', #17026, #22932, #13163 ) ;
#16881=PLANE ( 'NONE',  #3816 ) ;
#16902=ADVANCED_FACE ( 'NONE', ( #22860 ), #1343, .F. ) ;
#16903=DIRECTION ( 'NONE',  ( 9.999999999999998805E-16, -0.9439899321577399638, -0.3299742535180969494 ) ) ;
#16949=EDGE_CURVE ( 'NONE', #16232, #2876, #19621, .T. ) ;
#16952=ORIENTED_EDGE ( 'NONE', *, *, #15800, .F. ) ;
#16956=DIRECTION ( 'NONE',  ( 0.000000000000000000, -0.3299742535180974490, 0.9439899321577398528 ) ) ;
#16968=EDGE_LOOP ( 'NONE', ( #24855, #4200, #421, #17095 ) ) ;
#17026=CARTESIAN_POINT ( 'NONE',  ( 43.31606138205700063, -12.97731741051367393, 21.08248588348817876 ) ) ;
#17042=CARTESIAN_POINT ( 'NONE',  ( 36.31606138205700773, -20.93502329652820038, 27.89939821807130826 ) ) ;
#17095=ORIENTED_EDGE ( 'NONE', *, *, #9151, .T. ) ;
#17103=EDGE_CURVE ( 'NONE', #20448, #18554, #5955, .T. ) ;
#17125=ORIENTED_EDGE ( 'NONE', *, *, #3339, .F. ) ;
#17135=( NAMED_UNIT ( * ) SI_UNIT ( $, .STERADIAN. ) SOLID_ANGLE_UNIT ( ) );
#17156=VECTOR ( 'NONE', #24519, 1000.000000000000000 ) ;
#17212=AXIS2_PLACEMENT_3D ( 'NONE', #24286, #7173, #16956 ) ;
#17214=CARTESIAN_POINT ( 'NONE',  ( 37.14448850680319936, -22.27515649656511698, 29.48506754039016542 ) ) ;
#17216=VERTEX_POINT ( 'NONE', #3115 ) ;
#17245=ORIENTED_EDGE ( 'NONE', *, *, #12563, .T. ) ;
#17270=CARTESIAN_POINT ( 'NONE',  ( 40.31606138205700773, -19.28757846107943763, 24.56123906878952567 ) ) ;
#17290=ADVANCED_FACE ( 'NONE', ( #7118 ), #6172, .T. ) ;
#17380=DIRECTION ( 'NONE',  ( -7.071067811865477305E-16, 0.4341746501209515774, 0.9008287146801823297 ) ) ;
#17382=EDGE_CURVE ( 'NONE', #24915, #1030, #1810, .T. ) ;
#17390=DIRECTION ( 'NONE',  ( 1.000000000000000000, 1.000000000000000078E-15, 0.000000000000000000 ) ) ;
#17420=DIRECTION ( 'NONE',  ( 0.000000000000000000, 0.3299742535180963943, -0.9439899321577402969 ) ) ;
#17425=AXIS2_PLACEMENT_3D ( 'NONE', #3078, #22666, #10823 ) ;
#17445=DIRECTION ( 'NONE',  ( 1.218693434051482139E-16, -0.4425581086832393041, 0.8967398287344630070 ) ) ;
#17467=DIRECTION ( 'NONE',  ( -1.000000000000000000, -1.000000000000000078E-15, 0.000000000000000000 ) ) ;
#17472=PLANE ( 'NONE',  #4803 ) ;
#17509=VERTEX_POINT ( 'NONE', #22285 ) ;
#17519=DIRECTION ( 'NONE',  ( -1.000000000000000000, -1.000000000000000078E-15, 0.000000000000000000 ) ) ;
#17566=DIRECTION ( 'NONE',  ( -9.999999999999998805E-16, 0.9439899321577399638, 0.3299742535180969494 ) ) ;
#17682=CYLINDRICAL_SURFACE ( 'NONE', #6706, 1.250000000000000888 ) ;
#17721=CARTESIAN_POINT ( 'NONE',  ( 38.31606138205700773, -21.82678658219787948, 29.70634659473178019 ) ) ;
#17756=EDGE_CURVE ( 'NONE', #2232, #13035, #20326, .T. ) ;
#17777=AXIS2_PLACEMENT_3D ( 'NONE', #8674, #18452, #2713 ) ;
#17806=CARTESIAN_POINT ( 'NONE',  ( 43.31606138205700063, -12.40281258615395465, 20.95421293576468358 ) ) ;
#17808=CARTESIAN_POINT ( 'NONE',  ( 36.31606138205700773, -19.47805968271055477, 24.94720442500192448 ) ) ;
#17816=CARTESIAN_POINT ( 'NONE',  ( 43.31606138205700773, -18.80550481115970740, 25.27912300651437150 ) ) ;
#17833=CARTESIAN_POINT ( 'NONE',  ( 40.31606138205700773, -13.58280000135113319, 20.54174511886706256 ) ) ;
#17857=ORIENTED_EDGE ( 'NONE', *, *, #3339, .T. ) ;
#17861=ORIENTED_EDGE ( 'NONE', *, *, #12176, .T. ) ;
#17889=APPLICATION_CONTEXT ( 'automotive_design' ) ;
#17904=EDGE_CURVE ( 'NONE', #126, #2876, #5371, .T. ) ;
#17912=( NAMED_UNIT ( * ) SI_UNIT ( $, .STERADIAN. ) SOLID_ANGLE_UNIT ( ) );
#17933=EDGE_CURVE ( 'NONE', #3377, #5254, #22881, .T. ) ;
#18009=PLANE ( 'NONE',  #24996 ) ;
#18013=VECTOR ( 'NONE', #23866, 1000.000000000000000 ) ;
#18048=LINE ( 'NONE', #4266, #2486 ) ;
#18065=CARTESIAN_POINT ( 'NONE',  ( 43.31606138205700063, -13.58280000135112964, 20.54174511886706256 ) ) ;
#18069=DIRECTION ( 'NONE',  ( 0.000000000000000000, -0.3299742535180970049, 0.9439899321577400748 ) ) ;
#18074=EDGE_CURVE ( 'NONE', #18554, #13035, #13477, .T. ) ;
#18104=CARTESIAN_POINT ( 'NONE',  ( 36.31606138205700063, -11.51539968388052060, 18.41550321377400934 ) ) ;
#18121=DIRECTION ( 'NONE',  ( 1.000000000000000000, 1.156482317317870344E-15, 0.000000000000000000 ) ) ;
#18128=EDGE_LOOP ( 'NONE', ( #7476, #23381, #5584, #7182, #18418, #9486, #23096, #23643, #24560, #18879, #11750 ) ) ;
#18137=DIRECTION ( 'NONE',  ( 0.000000000000000000, -0.3299742535180970049, 0.9439899321577400748 ) ) ;
#18187=DIRECTION ( 'NONE',  ( 7.071067811865491110E-16, -0.9008287146801832179, 0.4341746501209495790 ) ) ;
#18202=ORIENTED_EDGE ( 'NONE', *, *, #12854, .F. ) ;
#18302=LINE ( 'NONE', #8384, #13619 ) ;
#18310=CARTESIAN_POINT ( 'NONE',  ( 36.31606138205700063, -13.04008168869994932, 21.66778101221729713 ) ) ;
#18336=DIRECTION ( 'NONE',  ( -1.000000000000000000, -1.000000000000000078E-15, 0.000000000000000000 ) ) ;
#18342=CARTESIAN_POINT ( 'NONE',  ( 36.31606138205700063, -10.66749763588700262, 14.47455635838400134 ) ) ;
#18350=DIRECTION ( 'NONE',  ( -1.000000000000000000, -1.000000000000000078E-15, 0.000000000000000000 ) ) ;
#18377=CARTESIAN_POINT ( 'NONE',  ( 38.31606138205700773, -22.27515649656512053, 29.48506754039017963 ) ) ;
#18398=EDGE_CURVE ( 'NONE', #8601, #19706, #23747, .T. ) ;
#18410=VECTOR ( 'NONE', #18187, 1000.000000000000227 ) ;
#18418=ORIENTED_EDGE ( 'NONE', *, *, #13971, .F. ) ;
#18452=DIRECTION ( 'NONE',  ( -1.000000000000000000, -1.000000000000000078E-15, 0.000000000000000000 ) ) ;
#18462=DIRECTION ( 'NONE',  ( 1.000000000000000000, 8.911169920151748851E-16, 3.114923731923493702E-16 ) ) ;
#18465=DIRECTION ( 'NONE',  ( 0.000000000000000000, -0.3299742535180970049, 0.9439899321577400748 ) ) ;
#18491=DIRECTION ( 'NONE',  ( 9.925461516413221718E-16, -0.8967398287344632291, -0.4425581086832394151 ) ) ;
#18499=VECTOR ( 'NONE', #13158, 1000.000000000000227 ) ;
#18521=VECTOR ( 'NONE', #24348, 1000.000000000000227 ) ;
#18541=UNCERTAINTY_MEASURE_WITH_UNIT (LENGTH_MEASURE( 1.000000000000000082E-05 ), #13905, 'distance_accuracy_value', 'NONE');
#18548=PLANE ( 'NONE',  #20074 ) ;
#18554=VERTEX_POINT ( 'NONE', #15808 ) ;
#18567=VERTEX_POINT ( 'NONE', #13758 ) ;
#18578=FACE_OUTER_BOUND ( 'NONE', #1339, .T. ) ;
#18594=CARTESIAN_POINT ( 'NONE',  ( 40.31606138205700773, -21.45740613484709769, 28.95788407061096237 ) ) ;
#18608=CARTESIAN_POINT ( 'NONE',  ( 36.31606138205700063, -11.51539968388052060, 18.41550321377400934 ) ) ;
#18651=CIRCLE ( 'NONE', #23986, 1.250000000000000888 ) ;
#18678=CARTESIAN_POINT ( 'NONE',  ( 40.31606138205701484, -19.34822312381089660, 24.15308711316412627 ) ) ;
#18740=ORIENTED_EDGE ( 'NONE', *, *, #5246, .T. ) ;
#18830=EDGE_LOOP ( 'NONE', ( #11657, #8443, #12167, #13745 ) ) ;
#18879=ORIENTED_EDGE ( 'NONE', *, *, #1421, .T. ) ;
#18884=FILL_AREA_STYLE_COLOUR ( '', #19093 ) ;
#18886=VECTOR ( 'NONE', #16525, 1000.000000000000227 ) ;
#18926=EDGE_LOOP ( 'NONE', ( #3812, #20291, #23359, #2887 ) ) ;
#18940=( NAMED_UNIT ( * ) PLANE_ANGLE_UNIT ( ) SI_UNIT ( $, .RADIAN. ) );
#18994=ORIENTED_EDGE ( 'NONE', *, *, #21377, .F. ) ;
#19051=VECTOR ( 'NONE', #9763, 1000.000000000000227 ) ;
#19063=CARTESIAN_POINT ( 'NONE',  ( 36.31606138205700063, -10.19550266980813369, 14.63954348514304904 ) ) ;
#19093=COLOUR_RGB ( '', 0.66274510, 0.83137255, 0.94901961) ;
#19131=ORIENTED_EDGE ( 'NONE', *, *, #18398, .F. ) ;
#19217=FACE_OUTER_BOUND ( 'NONE', #15579, .T. ) ;
#19235=FACE_OUTER_BOUND ( 'NONE', #8901, .T. ) ;
#19290=DIRECTION ( 'NONE',  ( 0.000000000000000000, -0.3299742535180970049, 0.9439899321577400748 ) ) ;
#19298=VECTOR ( 'NONE', #17, 1000.000000000000114 ) ;
#19316=CARTESIAN_POINT ( 'NONE',  ( 36.31606138205700063, -11.98739464995938953, 18.25051608701495809 ) ) ;
#19318=AXIS2_PLACEMENT_3D ( 'NONE', #23344, #11780, #11653 ) ;
#19343=CARTESIAN_POINT ( 'NONE',  ( 40.31606138205701484, -21.83924545618508617, 28.60179643084732604 ) ) ;
#19368=ADVANCED_FACE ( 'NONE', ( #10273 ), #18009, .F. ) ;
#19392=ORIENTED_EDGE ( 'NONE', *, *, #4401, .T. ) ;
#19422=LINE ( 'NONE', #15822, #21065 ) ;
#19451=EDGE_CURVE ( 'NONE', #17509, #3532, #10146, .T. ) ;
#19457=CARTESIAN_POINT ( 'NONE',  ( 33.31606138205700773, -19.34822312381090370, 24.15308711316412627 ) ) ;
#19473=AXIS2_PLACEMENT_3D ( 'NONE', #3615, #15471, #13303 ) ;
#19506=EDGE_CURVE ( 'NONE', #2232, #8221, #24283, .T. ) ;
#19538=VECTOR ( 'NONE', #18336, 1000.000000000000000 ) ;
#19552=DIRECTION ( 'NONE',  ( 1.000000000000000000, 1.156482317317870344E-15, 0.000000000000000000 ) ) ;
#19559=LINE ( 'NONE', #21748, #11616 ) ;
#19602=CARTESIAN_POINT ( 'NONE',  ( 33.31606138205700773, -13.58280000135114030, 20.54174511886706256 ) ) ;
#19613=CARTESIAN_POINT ( 'NONE',  ( 43.31606138205700773, -18.80550481115970740, 25.27912300651437150 ) ) ;
#19617=DIRECTION ( 'NONE',  ( -1.000000000000000078E-15, 0.9439899321577400748, 0.3299742535180970049 ) ) ;
#19621=LINE ( 'NONE', #12042, #15401 ) ;
#19679=PLANE ( 'NONE',  #14422 ) ;
#19701=VECTOR ( 'NONE', #18350, 1000.000000000000000 ) ;
#19705=ORIENTED_EDGE ( 'NONE', *, *, #19506, .T. ) ;
#19706=VERTEX_POINT ( 'NONE', #1597 ) ;
#19730=DIRECTION ( 'NONE',  ( 9.925461516413219746E-16, -0.8967398287344630070, -0.4425581086832393041 ) ) ;
#19757=AXIS2_PLACEMENT_3D ( 'NONE', #16479, #253, #10574 ) ;
#19769=DIRECTION ( 'NONE',  ( -1.000000000000000078E-15, 0.9439899321577400748, 0.3299742535180970049 ) ) ;
#19827=ADVANCED_FACE ( 'NONE', ( #2241 ), #7802, .F. ) ;
#19883=PLANE ( 'NONE',  #9659 ) ;
#19886=VECTOR ( 'NONE', #3770, 1000.000000000000227 ) ;
#19889=DIRECTION ( 'NONE',  ( -9.925461516413221718E-16, 0.8967398287344632291, 0.4425581086832394151 ) ) ;
#19902=DIRECTION ( 'NONE',  ( 9.999999999999998805E-16, -0.9439899321577399638, -0.3299742535180969494 ) ) ;
#19907=ORIENTED_EDGE ( 'NONE', *, *, #16312, .F. ) ;
#19911=VERTEX_POINT ( 'NONE', #14233 ) ;
#19924=DIRECTION ( 'NONE',  ( 7.071067811865491110E-16, -0.9008287146801832179, 0.4341746501209495790 ) ) ;
#19945=ORIENTED_EDGE ( 'NONE', *, *, #20664, .F. ) ;
#19973=EDGE_CURVE ( 'NONE', #15276, #3312, #4186, .T. ) ;
#19975=CARTESIAN_POINT ( 'NONE',  ( 36.31606138205700773, -20.93502329652820038, 27.89939821807130826 ) ) ;
#20016=ORIENTED_EDGE ( 'NONE', *, *, #8801, .T. ) ;
#20044=EDGE_CURVE ( 'NONE', #12956, #10061, #11482, .T. ) ;
#20057=CARTESIAN_POINT ( 'NONE',  ( 40.31606138205700773, -11.51539968388051705, 18.41550321377400934 ) ) ;
#20074=AXIS2_PLACEMENT_3D ( 'NONE', #12635, #10820, #12888 ) ;
#20104=EDGE_CURVE ( 'NONE', #4547, #14366, #24494, .T. ) ;
#20106=EDGE_CURVE ( 'NONE', #15148, #8601, #10496, .T. ) ;
#20124=ORIENTED_EDGE ( 'NONE', *, *, #8960, .F. ) ;
#20129=CIRCLE ( 'NONE', #356, 0.7500000000000008882 ) ;
#20151=AXIS2_PLACEMENT_3D ( 'NONE', #6556, #20347, #14418 ) ;
#20156=CARTESIAN_POINT ( 'NONE',  ( 43.31606138205700063, -12.40281258615395465, 20.95421293576468358 ) ) ;
#20209=SURFACE_STYLE_USAGE ( .BOTH. , #12235 ) ;
#20222=CARTESIAN_POINT ( 'NONE',  ( 43.31606138205700773, -19.13113579875041381, 24.60350147050422720 ) ) ;
#20252=VERTEX_POINT ( 'NONE', #23211 ) ;
#20282=CARTESIAN_POINT ( 'NONE',  ( 39.48763425731081611, -21.82678658219787948, 29.70634659473178374 ) ) ;
#20291=ORIENTED_EDGE ( 'NONE', *, *, #12616, .F. ) ;
#20300=VECTOR ( 'NONE', #14086, 1000.000000000000000 ) ;
#20307=AXIS2_PLACEMENT_3D ( 'NONE', #12933, #12561, #18465 ) ;
#20325=ORIENTED_EDGE ( 'NONE', *, *, #20106, .F. ) ;
#20326=LINE ( 'NONE', #12352, #5029 ) ;
#20347=DIRECTION ( 'NONE',  ( 4.341746501209495972E-16, -0.4341746501209495790, -0.9008287146801833289 ) ) ;
#20358=FACE_OUTER_BOUND ( 'NONE', #2095, .T. ) ;
#20388=PLANE ( 'NONE',  #5069 ) ;
#20393=DIRECTION ( 'NONE',  ( -1.000000000000000000, -1.000000000000000078E-15, 0.000000000000000000 ) ) ;
#20436=ADVANCED_FACE ( 'NONE', ( #15868 ), #12156, .T. ) ;
#20448=VERTEX_POINT ( 'NONE', #11771 ) ;
#20458=LINE ( 'NONE', #8878, #9989 ) ;
#20479=ORIENTED_EDGE ( 'NONE', *, *, #14916, .T. ) ;
#20483=ORIENTED_EDGE ( 'NONE', *, *, #13906, .T. ) ;
#20484=CYLINDRICAL_SURFACE ( 'NONE', #19757, 3.000000000000002665 ) ;
#20490=CIRCLE ( 'NONE', #17212, 1.250000000000000888 ) ;
#20502=EDGE_CURVE ( 'NONE', #15148, #20448, #265, .T. ) ;
#20546=ORIENTED_EDGE ( 'NONE', *, *, #12093, .F. ) ;
#20547=LINE ( 'NONE', #24266, #23495 ) ;
#20564=CARTESIAN_POINT ( 'NONE',  ( 43.31606138205700773, -19.13113579875041381, 24.60350147050422720 ) ) ;
#20587=ADVANCED_BREP_SHAPE_REPRESENTATION ( '', ( #8266, #2000 ), #2615 ) ;
#20627=EDGE_LOOP ( 'NONE', ( #5463, #11103, #2284, #11422, #14333, #289, #12611, #22846, #24030, #21899 ) ) ;
#20645=DIRECTION ( 'NONE',  ( -9.925461516413211857E-16, 0.8967398287344598984, 0.4425581086832454658 ) ) ;
#20648=ORIENTED_EDGE ( 'NONE', *, *, #20754, .F. ) ;
#20652=PRODUCT_DEFINITION ( 'UNKNOWN', '', #16631, #24944 ) ;
#20664=EDGE_CURVE ( 'NONE', #11095, #828, #772, .T. ) ;
#20685=ORIENTED_EDGE ( 'NONE', *, *, #12616, .T. ) ;
#20719=VECTOR ( 'NONE', #10949, 1000.000000000000227 ) ;
#20754=EDGE_CURVE ( 'NONE', #23347, #24520, #11355, .T. ) ;
#20776=ORIENTED_EDGE ( 'NONE', *, *, #20106, .T. ) ;
#20800=DIRECTION ( 'NONE',  ( 0.000000000000000000, 0.3299742535180963943, -0.9439899321577402969 ) ) ;
#20810=DIRECTION ( 'NONE',  ( -1.000000000000000000, -1.000000000000000078E-15, 0.000000000000000000 ) ) ;
#20867=FILL_AREA_STYLE ('',( #8902 ) ) ;
#20872=DIRECTION ( 'NONE',  ( 0.000000000000000000, -0.3299742535180970049, 0.9439899321577400748 ) ) ;
#20884=EDGE_CURVE ( 'NONE', #24591, #1030, #1533, .T. ) ;
#20958=ORIENTED_EDGE ( 'NONE', *, *, #2908, .F. ) ;
#20989=VECTOR ( 'NONE', #23713, 1000.000000000000227 ) ;
#20991=FACE_OUTER_BOUND ( 'NONE', #2865, .T. ) ;
#20997=LINE ( 'NONE', #19063, #24430 ) ;
#21058=LINE ( 'NONE', #3401, #2218 ) ;
#21063=CARTESIAN_POINT ( 'NONE',  ( 33.31606138205700773, -18.80550481115971806, 25.27912300651437150 ) ) ;
#21065=VECTOR ( 'NONE', #9664, 1000.000000000000227 ) ;
#21074=ADVANCED_FACE ( 'NONE', ( #14292 ), #22141, .F. ) ;
#21078=EDGE_LOOP ( 'NONE', ( #16228, #24561, #1802, #3544 ) ) ;
#21081=DIRECTION ( 'NONE',  ( 4.341746501209495972E-16, -0.4341746501209495790, -0.9008287146801833289 ) ) ;
#21115=UNCERTAINTY_MEASURE_WITH_UNIT (LENGTH_MEASURE( 1.000000000000000082E-05 ), #22616, 'distance_accuracy_value', 'NONE');
#21179=CARTESIAN_POINT ( 'NONE',  ( 43.31606138205700063, -13.04008168869994222, 21.66778101221729713 ) ) ;
#21181=DIRECTION ( 'NONE',  ( 0.000000000000000000, 0.3299742535180974490, -0.9439899321577398528 ) ) ;
#21247=ORIENTED_EDGE ( 'NONE', *, *, #15612, .T. ) ;
#21250=ADVANCED_FACE ( 'NONE', ( #7204 ), #22902, .F. ) ;
#21321=CARTESIAN_POINT ( 'NONE',  ( 43.31606138205700063, -12.76023008545320181, 21.53290024082827969 ) ) ;
#21333=CARTESIAN_POINT ( 'NONE',  ( 39.48763425731081611, -21.82678658219787593, 29.70634659473178374 ) ) ;
#21342=ORIENTED_EDGE ( 'NONE', *, *, #14464, .F. ) ;
#21344=CARTESIAN_POINT ( 'NONE',  ( 36.31606138205700063, -12.40281258615396176, 20.95421293576468358 ) ) ;
#21368=EDGE_LOOP ( 'NONE', ( #21555, #21474, #10016, #2741 ) ) ;
#21377=EDGE_CURVE ( 'NONE', #19911, #11722, #12310, .T. ) ;
#21384=EDGE_CURVE ( 'NONE', #7327, #23347, #3985, .T. ) ;
#21402=FACE_OUTER_BOUND ( 'NONE', #2640, .T. ) ;
#21407=DIRECTION ( 'NONE',  ( -9.925461516413211857E-16, 0.8967398287344600094, 0.4425581086832455213 ) ) ;
#21408=EDGE_CURVE ( 'NONE', #12627, #9628, #12187, .T. ) ;
#21464=CARTESIAN_POINT ( 'NONE',  ( 40.31606138205700773, -21.45740613484709769, 28.95788407061096237 ) ) ;
#21474=ORIENTED_EDGE ( 'NONE', *, *, #17904, .F. ) ;
#21489=DIRECTION ( 'NONE',  ( 1.000000000000000000, 1.000000000000000078E-15, 0.000000000000000000 ) ) ;
#21518=ORIENTED_EDGE ( 'NONE', *, *, #17382, .T. ) ;
#21521=VECTOR ( 'NONE', #1579, 1000.000000000000227 ) ;
#21533=FACE_OUTER_BOUND ( 'NONE', #1478, .T. ) ;
#21539=CARTESIAN_POINT ( 'NONE',  ( 37.14448850680319225, -22.27515649656511698, 29.48506754039016897 ) ) ;
#21555=ORIENTED_EDGE ( 'NONE', *, *, #11638, .F. ) ;
#21587=ORIENTED_EDGE ( 'NONE', *, *, #4765, .F. ) ;
#21597=EDGE_LOOP ( 'NONE', ( #21587, #11215, #15911, #400 ) ) ;
#21603=AXIS2_PLACEMENT_3D ( 'NONE', #9063, #24736, #24477 ) ;
#21693=ORIENTED_EDGE ( 'NONE', *, *, #20104, .F. ) ;
#21694=CIRCLE ( 'NONE', #4433, 3.000000000000002665 ) ;
#21741=ORIENTED_EDGE ( 'NONE', *, *, #4304, .F. ) ;
#21744=ORIENTED_EDGE ( 'NONE', *, *, #16949, .F. ) ;
#21746=VECTOR ( 'NONE', #3646, 1000.000000000000000 ) ;
#21748=CARTESIAN_POINT ( 'NONE',  ( 33.31606138205700773, -19.28757846107944474, 24.56123906878952567 ) ) ;
#21751=ORIENTED_EDGE ( 'NONE', *, *, #8457, .T. ) ;
#21761=( NAMED_UNIT ( * ) PLANE_ANGLE_UNIT ( ) SI_UNIT ( $, .RADIAN. ) );
#21766=AXIS2_PLACEMENT_3D ( 'NONE', #12939, #1062, #16397 ) ;
#21767=( BOUNDED_CURVE ( )  B_SPLINE_CURVE ( 3, ( #7307, #11045, #1373, #9259 ),
 .UNSPECIFIED., .F., .T. ) 
 B_SPLINE_CURVE_WITH_KNOTS ( ( 4, 4 ),
 ( 4.712388980384689674, 6.283185307179590673 ),
 .UNSPECIFIED. ) 
 CURVE ( )  GEOMETRIC_REPRESENTATION_ITEM ( )  RATIONAL_B_SPLINE_CURVE ( ( 1.000000000000000000, 0.8047378541243649375, 0.8047378541243649375, 1.000000000000000000 ) ) 
 REPRESENTATION_ITEM ( '' )  );
#21839=DIRECTION ( 'NONE',  ( 7.071067811865477305E-16, -0.4341746501209515774, -0.9008287146801823297 ) ) ;
#21851=LINE ( 'NONE', #6735, #2945 ) ;
#21899=ORIENTED_EDGE ( 'NONE', *, *, #15190, .F. ) ;
#21910=CYLINDRICAL_SURFACE ( 'NONE', #14409, 1.250000000000000888 ) ;
#21921=CARTESIAN_POINT ( 'NONE',  ( 40.31606138205700773, -13.58280000135113319, 20.54174511886706256 ) ) ;
#21984=ORIENTED_EDGE ( 'NONE', *, *, #7129, .T. ) ;
#22034=ADVANCED_FACE ( 'NONE', ( #9052 ), #9179, .T. ) ;
#22044=DIRECTION ( 'NONE',  ( 0.000000000000000000, 0.3299742535180974490, -0.9439899321577398528 ) ) ;
#22141=PLANE ( 'NONE',  #20151 ) ;
#22170=CARTESIAN_POINT ( 'NONE',  ( 43.31606138205700063, -11.18542543036241632, 17.47151328161626793 ) ) ;
#22186=VECTOR ( 'NONE', #7230, 1000.000000000000114 ) ;
#22206=CARTESIAN_POINT ( 'NONE',  ( 40.31606138205701484, -20.93502329652820038, 27.89939821807130826 ) ) ;
#22268=ORIENTED_EDGE ( 'NONE', *, *, #4558, .T. ) ;
#22285=CARTESIAN_POINT ( 'NONE',  ( 33.31606138205700773, -19.47805968271055477, 24.94720442500192448 ) ) ;
#22366=VECTOR ( 'NONE', #13527, 1000.000000000000227 ) ;
#22367=DIRECTION ( 'NONE',  ( 1.000000000000000000, 8.911169920151748851E-16, 3.114923731923493702E-16 ) ) ;
#22374=CARTESIAN_POINT ( 'NONE',  ( 40.31606138205701484, -20.93502329652820038, 27.89939821807130826 ) ) ;
#22386=VECTOR ( 'NONE', #21839, 1000.000000000000000 ) ;
#22416=DIRECTION ( 'NONE',  ( 0.000000000000000000, 0.3299742535180974490, -0.9439899321577398528 ) ) ;
#22450=ORIENTED_EDGE ( 'NONE', *, *, #9727, .T. ) ;
#22483=ADVANCED_FACE ( 'NONE', ( #15551 ), #9273, .F. ) ;
#22533=EDGE_CURVE ( 'NONE', #12836, #20252, #3277, .T. ) ;
#22537=DIRECTION ( 'NONE',  ( 1.000000000000000000, 0.000000000000000000, 0.000000000000000000 ) ) ;
#22551=CARTESIAN_POINT ( 'NONE',  ( 40.31606138205700773, -11.51539968388051705, 18.41550321377400934 ) ) ;
#22554=VECTOR ( 'NONE', #10907, 1000.000000000000227 ) ;
#22566=CARTESIAN_POINT ( 'NONE',  ( 33.31606138205700773, -11.18542543036242698, 17.47151328161626793 ) ) ;
#22616=( LENGTH_UNIT ( ) NAMED_UNIT ( * ) SI_UNIT ( .MILLI., .METRE. ) );
#22662=CARTESIAN_POINT ( 'NONE',  ( 43.31606138205700773, -19.92642959707777806, 24.72592537066031682 ) ) ;
#22666=DIRECTION ( 'NONE',  ( -1.000000000000000000, -1.052872940142565459E-15, -1.848188032574765003E-17 ) ) ;
#22692=ORIENTED_EDGE ( 'NONE', *, *, #25372, .F. ) ;
#22721=DIRECTION ( 'NONE',  ( -1.000000000000000000, -1.000000000000000078E-15, 0.000000000000000000 ) ) ;
#22765=AXIS2_PLACEMENT_3D ( 'NONE', #17816, #15744, #10085 ) ;
#22777=ADVANCED_FACE ( 'NONE', ( #23912 ), #7970, .T. ) ;
#22811=ORIENTED_EDGE ( 'NONE', *, *, #4401, .F. ) ;
#22827=LINE ( 'NONE', #12671, #15337 ) ;
#22846=ORIENTED_EDGE ( 'NONE', *, *, #4479, .T. ) ;
#22856=DIRECTION ( 'NONE',  ( 0.000000000000000000, -0.3299742535180969494, 0.9439899321577399638 ) ) ;
#22860=FACE_OUTER_BOUND ( 'NONE', #5455, .T. ) ;
#22881=LINE ( 'NONE', #16703, #2131 ) ;
#22893=DIRECTION ( 'NONE',  ( 0.000000000000000000, 0.4425581086832400257, -0.8967398287344627850 ) ) ;
#22897=EDGE_CURVE ( 'NONE', #5254, #7327, #24790, .T. ) ;
#22902=CYLINDRICAL_SURFACE ( 'NONE', #378, 2.000000000000001776 ) ;
#22923=EDGE_CURVE ( 'NONE', #7089, #18567, #14764, .T. ) ;
#22932=DIRECTION ( 'NONE',  ( 4.341746501209495972E-16, -0.4341746501209495790, -0.9008287146801833289 ) ) ;
#22974=CARTESIAN_POINT ( 'NONE',  ( 43.31606138205700773, -19.47805968271054766, 24.94720442500192448 ) ) ;
#22978=ORIENTED_EDGE ( 'NONE', *, *, #18074, .T. ) ;
#22980=CYLINDRICAL_SURFACE ( 'NONE', #8348, 0.7500000000000008882 ) ;
#22994=ORIENTED_EDGE ( 'NONE', *, *, #15098, .F. ) ;
#23020=DIRECTION ( 'NONE',  ( 8.967398287344632705E-16, -0.8967398287344631180, -0.4425581086832391375 ) ) ;
#23096=ORIENTED_EDGE ( 'NONE', *, *, #20754, .T. ) ;
#23109=ORIENTED_EDGE ( 'NONE', *, *, #17756, .F. ) ;
#23157=DIRECTION ( 'NONE',  ( 1.000000000000000275E-15, -0.9439899321577401858, -0.3299742535180970604 ) ) ;
#23167=LINE ( 'NONE', #9410, #3221 ) ;
#23199=CARTESIAN_POINT ( 'NONE',  ( 38.31606138205700773, -21.82678658219787948, 29.70634659473178019 ) ) ;
#23211=CARTESIAN_POINT ( 'NONE',  ( 40.31606138205700773, -10.19550266980813014, 14.63954348514304904 ) ) ;
#23252=EDGE_LOOP ( 'NONE', ( #21741, #13069, #5842, #5396 ) ) ;
#23259=ORIENTED_EDGE ( 'NONE', *, *, #23552, .F. ) ;
#23304=ADVANCED_FACE ( 'NONE', ( #13726 ), #13875, .T. ) ;
#23344=CARTESIAN_POINT ( 'NONE',  ( 38.31606138205700063, -11.51539968388051882, 18.41550321377400934 ) ) ;
#23347=VERTEX_POINT ( 'NONE', #16527 ) ;
#23350=DIRECTION ( 'NONE',  ( 1.000000000000000000, 8.911169920151748851E-16, 3.114923731923493702E-16 ) ) ;
#23359=ORIENTED_EDGE ( 'NONE', *, *, #13519, .F. ) ;
#23367=EDGE_LOOP ( 'NONE', ( #162, #8769, #15374, #9902 ) ) ;
#23381=ORIENTED_EDGE ( 'NONE', *, *, #20044, .T. ) ;
#23409=EDGE_CURVE ( 'NONE', #17216, #16296, #11357, .T. ) ;
#23420=ADVANCED_FACE ( 'NONE', ( #24247 ), #807, .T. ) ;
#23447=ORIENTED_EDGE ( 'NONE', *, *, #12093, .T. ) ;
#23448=FACE_OUTER_BOUND ( 'NONE', #15144, .T. ) ;
#23495=VECTOR ( 'NONE', #10513, 1000.000000000000227 ) ;
#23516=CIRCLE ( 'NONE', #13255, 3.000000000000002665 ) ;
#23540=AXIS2_PLACEMENT_3D ( 'NONE', #9540, #7861, #25218 ) ;
#23552=EDGE_CURVE ( 'NONE', #30, #3261, #5549, .T. ) ;
#23588=LINE ( 'NONE', #23710, #13058 ) ;
#23604=MECHANICAL_DESIGN_GEOMETRIC_PRESENTATION_REPRESENTATION('',(#25242),#4291);
#23611=LINE ( 'NONE', #7401, #19886 ) ;
#23619=DIRECTION ( 'NONE',  ( 0.000000000000000000, -0.3299742535180970049, 0.9439899321577400748 ) ) ;
#23643=ORIENTED_EDGE ( 'NONE', *, *, #5700, .T. ) ;
#23661=ORIENTED_EDGE ( 'NONE', *, *, #9151, .F. ) ;
#23686=DIRECTION ( 'NONE',  ( 0.000000000000000000, 0.3299742535180974490, -0.9439899321577398528 ) ) ;
#23710=CARTESIAN_POINT ( 'NONE',  ( 36.31606138205700063, -12.76023008545320714, 21.53290024082827969 ) ) ;
#23713=DIRECTION ( 'NONE',  ( 0.000000000000000000, -0.3299742535180969494, 0.9439899321577399638 ) ) ;
#23747=CIRCLE ( 'NONE', #5260, 2.999999999999998668 ) ;
#23796=CARTESIAN_POINT ( 'NONE',  ( 40.31606138205700773, -12.87480755223282713, 20.78922580900563588 ) ) ;
#23798=VECTOR ( 'NONE', #19902, 1000.000000000000227 ) ;
#23836=CARTESIAN_POINT ( 'NONE',  ( 40.31606138205700773, -12.76023008545320359, 21.53290024082827969 ) ) ;
#23853=AXIS2_PLACEMENT_3D ( 'NONE', #14578, #2970, #4919 ) ;
#23866=DIRECTION ( 'NONE',  ( -1.000000000000000000, -1.000000000000000078E-15, 0.000000000000000000 ) ) ;
#23870=CARTESIAN_POINT ( 'NONE',  ( 43.31606138205700063, -13.04008168869994222, 21.66778101221729713 ) ) ;
#23888=UNCERTAINTY_MEASURE_WITH_UNIT (LENGTH_MEASURE( 1.000000000000000082E-05 ), #1018, 'distance_accuracy_value', 'NONE');
#23912=FACE_OUTER_BOUND ( 'NONE', #2836, .T. ) ;
#23924=ORIENTED_EDGE ( 'NONE', *, *, #14916, .F. ) ;
#23932=PRESENTATION_STYLE_ASSIGNMENT (( #20209 ) ) ;
#23965=VECTOR ( 'NONE', #6408, 1000.000000000000000 ) ;
#23973=CIRCLE ( 'NONE', #16574, 0.7500000000000008882 ) ;
#23978=CARTESIAN_POINT ( 'NONE',  ( 43.31606138205700063, -10.66749763588699551, 14.47455635838400134 ) ) ;
#23986=AXIS2_PLACEMENT_3D ( 'NONE', #21921, #5829, #5961 ) ;
#24030=ORIENTED_EDGE ( 'NONE', *, *, #12854, .T. ) ;
#24033=AXIS2_PLACEMENT_3D ( 'NONE', #6736, #19889, #12295 ) ;
#24062=( NAMED_UNIT ( * ) PLANE_ANGLE_UNIT ( ) SI_UNIT ( $, .RADIAN. ) );
#24115=ADVANCED_FACE ( 'NONE', ( #15433 ), #19679, .F. ) ;
#24136=CARTESIAN_POINT ( 'NONE',  ( 43.31606138205700063, -12.40281258615395465, 20.95421293576468358 ) ) ;
#24142=VECTOR ( 'NONE', #16029, 1000.000000000000227 ) ;
#24164=ORIENTED_EDGE ( 'NONE', *, *, #20884, .T. ) ;
#24237=ORIENTED_EDGE ( 'NONE', *, *, #10067, .T. ) ;
#24247=FACE_OUTER_BOUND ( 'NONE', #4606, .T. ) ;
#24266=CARTESIAN_POINT ( 'NONE',  ( 43.31606138205700063, -13.25716901376041967, 21.21736665487721041 ) ) ;
#24283=LINE ( 'NONE', #9114, #22554 ) ;
#24285=CARTESIAN_POINT ( 'NONE',  ( 43.31606138205700773, -19.13113579875041381, 24.60350147050422720 ) ) ;
#24286=CARTESIAN_POINT ( 'NONE',  ( 43.31606138205700063, -13.58280000135112964, 20.54174511886706256 ) ) ;
#24338=CARTESIAN_POINT ( 'NONE',  ( 33.31606138205700773, -13.04008168869995288, 21.66778101221729713 ) ) ;
#24348=DIRECTION ( 'NONE',  ( -1.218693434051482139E-16, 0.4425581086832393041, -0.8967398287344630070 ) ) ;
#24368=CARTESIAN_POINT ( 'NONE',  ( 40.31606138205701484, -19.92642959707778516, 24.72592537066031682 ) ) ;
#24430=VECTOR ( 'NONE', #25212, 1000.000000000000227 ) ;
#24472=ORIENTED_EDGE ( 'NONE', *, *, #5700, .F. ) ;
#24473=LINE ( 'NONE', #24732, #18521 ) ;
#24477=DIRECTION ( 'NONE',  ( 0.000000000000000000, 0.4425581086832455213, -0.8967398287344598984 ) ) ;
#24478=DIRECTION ( 'NONE',  ( -1.000000000000000000, -1.000000000000000078E-15, 0.000000000000000000 ) ) ;
#24494=LINE ( 'NONE', #12569, #18886 ) ;
#24519=DIRECTION ( 'NONE',  ( -1.000000000000000000, -1.000000000000000078E-15, 0.000000000000000000 ) ) ;
#24520=VERTEX_POINT ( 'NONE', #22374 ) ;
#24529=DIRECTION ( 'NONE',  ( -1.000000000000000000, -1.000000000000000078E-15, 0.000000000000000000 ) ) ;
#24530=CARTESIAN_POINT ( 'NONE',  ( 40.31606138205700773, -11.51539968388051705, 18.41550321377400934 ) ) ;
#24560=ORIENTED_EDGE ( 'NONE', *, *, #4304, .T. ) ;
#24561=ORIENTED_EDGE ( 'NONE', *, *, #4643, .F. ) ;
#24591=VERTEX_POINT ( 'NONE', #7296 ) ;
#24713=CARTESIAN_POINT ( 'NONE',  ( 43.31606138205700773, -18.80550481115970740, 25.27912300651437150 ) ) ;
#24732=CARTESIAN_POINT ( 'NONE',  ( 36.31606138205700773, -19.73594837544667513, 24.33996001444790025 ) ) ;
#24736=DIRECTION ( 'NONE',  ( 9.925461516413211857E-16, -0.8967398287344600094, -0.4425581086832455213 ) ) ;
#24738=VECTOR ( 'NONE', #3618, 1000.000000000000000 ) ;
#24760=ORIENTED_EDGE ( 'NONE', *, *, #25440, .F. ) ;
#24787=AXIS2_PLACEMENT_3D ( 'NONE', #11006, #22721, #5210 ) ;
#24790=LINE ( 'NONE', #24285, #5349 ) ;
#24809=EDGE_CURVE ( 'NONE', #8986, #7089, #14441, .T. ) ;
#24842=SURFACE_STYLE_USAGE ( .BOTH. , #3208 ) ;
#24853=EDGE_LOOP ( 'NONE', ( #15181, #3227, #9223, #3966 ) ) ;
#24854=CARTESIAN_POINT ( 'NONE',  ( 33.31606138205700773, -12.87480755223283424, 20.78922580900563588 ) ) ;
#24855=ORIENTED_EDGE ( 'NONE', *, *, #10067, .F. ) ;
#24897=PLANE ( 'NONE',  #12641 ) ;
#24915=VERTEX_POINT ( 'NONE', #24923 ) ;
#24920=ORIENTED_EDGE ( 'NONE', *, *, #16792, .F. ) ;
#24923=CARTESIAN_POINT ( 'NONE',  ( 36.31606138205700063, -12.40281258615396176, 20.95421293576468358 ) ) ;
#24931=FACE_OUTER_BOUND ( 'NONE', #9524, .T. ) ;
#24934=VECTOR ( 'NONE', #10138, 1000.000000000000227 ) ;
#24944=PRODUCT_DEFINITION_CONTEXT ( 'detailed design', #17889, 'design' ) ;
#24950=CARTESIAN_POINT ( 'NONE',  ( 33.31606138205700773, -19.34822312381090370, 24.15308711316412627 ) ) ;
#24960=LINE ( 'NONE', #10956, #8478 ) ;
#24996=AXIS2_PLACEMENT_3D ( 'NONE', #20057, #6410, #18137 ) ;
#25035=CARTESIAN_POINT ( 'NONE',  ( 36.31606138205700773, -21.90577604921434229, 28.73660501626934050 ) ) ;
#25048=ADVANCED_FACE ( 'NONE', ( #16045 ), #13865, .F. ) ;
#25075=VECTOR ( 'NONE', #1534, 1000.000000000000000 ) ;
#25096=ORIENTED_EDGE ( 'NONE', *, *, #9787, .T. ) ;
#25111=DIRECTION ( 'NONE',  ( 1.000000000000000000, 8.911169920151748851E-16, 3.114923731923493702E-16 ) ) ;
#25162=CARTESIAN_POINT ( 'NONE',  ( 33.31606138205700773, -12.40281258615396531, 20.95421293576468358 ) ) ;
#25191=EDGE_CURVE ( 'NONE', #9599, #3377, #20547, .T. ) ;
#25212=DIRECTION ( 'NONE',  ( -9.999999999999998805E-16, 0.9439899321577399638, 0.3299742535180969494 ) ) ;
#25218=DIRECTION ( 'NONE',  ( 1.000000000000000000, 1.156482317317870344E-15, 0.000000000000000000 ) ) ;
#25220=EDGE_CURVE ( 'NONE', #18567, #17509, #15688, .T. ) ;
#25234=ORIENTED_EDGE ( 'NONE', *, *, #20884, .F. ) ;
#25242=STYLED_ITEM ( 'NONE', ( #23932 ), #20587 ) ;
#25257=SHAPE_DEFINITION_REPRESENTATION ( #6233, #8505 ) ;
#25277=FACE_OUTER_BOUND ( 'NONE', #15781, .T. ) ;
#25288=EDGE_CURVE ( 'NONE', #12836, #12627, #1841, .T. ) ;
#25311=ORIENTED_EDGE ( 'NONE', *, *, #19973, .F. ) ;
#25357=ORIENTED_EDGE ( 'NONE', *, *, #5242, .T. ) ;
#25372=EDGE_CURVE ( 'NONE', #126, #9062, #13452, .T. ) ;
#25440=EDGE_CURVE ( 'NONE', #9628, #14366, #6690, .T. ) ;
#25450=CARTESIAN_POINT ( 'NONE',  ( 36.31606138205700773, -22.71854986786759412, 31.51329497139233737 ) ) ;
#25462=ORIENTED_EDGE ( 'NONE', *, *, #15098, .T. ) ;
ENDSEC;
END-ISO-10303-21;
